ISO-10303-21;
HEADER;
FILE_DESCRIPTION (('STEP AP214'),
    '1' );
FILE_NAME ('Self-Tapping Grease Fitting_8742T12.step',
    '2026-10-09T17:48:21',
    ( '' ),
    ( '' ),
    'SwSTEP 2.0',
    'SolidWorks 2024',
    '' );
FILE_SCHEMA (( 'AUTOMOTIVE_DESIGN' ));
ENDSEC;

DATA;
#3=CARTESIAN_POINT ( 'NONE',  ( 2.229831107420913838, -3.725624999999957776, -2.719112200499452126 ) ) ;
#9=CARTESIAN_POINT ( 'NONE',  ( 4.499999999999994671, 2.375000000000011102, -5.510910596163089556E-16 ) ) ;
#19=CARTESIAN_POINT ( 'NONE',  ( -3.913923972693154063, 0.4218750000000872080, 2.093842233512113626 ) ) ;
#21=CARTESIAN_POINT ( 'NONE',  ( -1.610069518889563289, -1.311713562373113096, -3.889976491222739252 ) ) ;
#30=LINE ( 'NONE', #2442, #6868 ) ;
#34=ORIENTED_EDGE ( 'NONE', *, *, #12854, .F. ) ;
#36=CARTESIAN_POINT ( 'NONE',  ( 1.804739227294467563, -4.171875000000069278, -3.379404665904198968 ) ) ;
#42=CARTESIAN_POINT ( 'NONE',  ( -1.024675879034753434, -5.362115055319378598, 3.196030698784670054 ) ) ;
#47=CARTESIAN_POINT ( 'NONE',  ( 3.443564157863920006, -5.257675013607999936, 0.5807209424340332715 ) ) ;
#53=EDGE_CURVE ( 'NONE', #8592, #3175, #10509, .T. ) ;
#54=ORIENTED_EDGE ( 'NONE', *, *, #8192, .T. ) ;
#56=CARTESIAN_POINT ( 'NONE',  ( 0.3421672931281763419, -3.819374999999898268, -3.487344533451359307 ) ) ;
#57=ORIENTED_EDGE ( 'NONE', *, *, #8169, .T. ) ;
#58=ORIENTED_EDGE ( 'NONE', *, *, #11069, .T. ) ;
#63=LINE ( 'NONE', #5245, #7516 ) ;
#67=CARTESIAN_POINT ( 'NONE',  ( -3.325293793763300698, -4.038125000000090559, -1.009645679448947231 ) ) ;
#75=CARTESIAN_POINT ( 'NONE',  ( -1.054465238365572599, -2.881875000000049702, -3.471494129216005753 ) ) ;
#82=CARTESIAN_POINT ( 'NONE',  ( 1.375881166777175254E-16, 9.250000000000000000, 0.000000000000000000 ) ) ;
#83=CARTESIAN_POINT ( 'NONE',  ( 5.196152422706631135, 0.1227504548087541975, -1.122964458370237425E-15 ) ) ;
#95=CARTESIAN_POINT ( 'NONE',  ( 0.4342252132666136744, 0.2343749999999768518, 4.392589664459995547 ) ) ;
#97=CARTESIAN_POINT ( 'NONE',  ( 0.8081574754459883714, -1.780463562373038489, 4.068519560952849723 ) ) ;
#111=DIRECTION ( 'NONE',  ( -0.7071067811865470176, -0.7071067811865481278, 0.000000000000000000 ) ) ;
#112=CARTESIAN_POINT ( 'NONE',  ( 0.001419932108912198322, -3.750000000000078160, 3.886924930609184869 ) ) ;
#114=B_SPLINE_CURVE_WITH_KNOTS ( 'NONE', 3,
 ( #8146, #5687, #3332, #849 ),
 .UNSPECIFIED., .F., .F.,
 ( 4, 4 ),
 ( 0.000000000000000000, 1.000000000000000000 ),
 .UNSPECIFIED. ) ;
#115=AXIS2_PLACEMENT_3D ( 'NONE', #6388, #13511, #12041 ) ;
#117=CARTESIAN_POINT ( 'NONE',  ( 3.639928100339127948, -0.5225000000000105116, 1.508827519571796172 ) ) ;
#118=CARTESIAN_POINT ( 'NONE',  ( 0.2965589474581596385, -5.389768145603638594, 3.307028203814240008 ) ) ;
#125=EDGE_CURVE ( 'NONE', #14595, #12756, #14394, .T. ) ;
#132=CARTESIAN_POINT ( 'NONE',  ( 2.822884439542550084, -2.694375000000075460, -2.318423337397389705 ) ) ;
#145=CARTESIAN_POINT ( 'NONE',  ( -3.897114317029972685, -9.945166405816852549E-15, -2.249999999999999112 ) ) ;
#148=CARTESIAN_POINT ( 'NONE',  ( 3.520079602834293109, -3.569375000000153619, 0.3476102605345692265 ) ) ;
#160=VERTEX_POINT ( 'NONE', #3006 ) ;
#162=CARTESIAN_POINT ( 'NONE',  ( -0.001340710925747373022, -2.834999999999994635, -3.634308738048381393 ) ) ;
#165=CARTESIAN_POINT ( 'NONE',  ( 2.937061643673781752, -5.103115294876279684, -2.234448363260541193 ) ) ;
#182=CARTESIAN_POINT ( 'NONE',  ( 2.923540125992261984, -1.874213562373038489, 2.925090027579059004 ) ) ;
#192=CARTESIAN_POINT ( 'NONE',  ( -1.106373576938931125, -4.296874999999863221, -3.650653549769442119 ) ) ;
#194=EDGE_CURVE ( 'NONE', #3175, #4923, #10253, .T. ) ;
#196=CARTESIAN_POINT ( 'NONE',  ( 3.459076575081923899, -0.6631250000000769029, -1.847748348019847109 ) ) ;
#198=CARTESIAN_POINT ( 'NONE',  ( -2.819918635305147525, -5.316771972388096401, 1.943909394665495727 ) ) ;
#210=CARTESIAN_POINT ( 'NONE',  ( 2.488663048653546372, -3.709999999999854303, -2.487386788893799938 ) ) ;
#222=CARTESIAN_POINT ( 'NONE',  ( 3.376561219002149450, -3.631875000000035048, -1.025635141340205836 ) ) ;
#229=ORIENTED_EDGE ( 'NONE', *, *, #14616, .F. ) ;
#230=EDGE_CURVE ( 'NONE', #5514, #2409, #14717, .T. ) ;
#231=CARTESIAN_POINT ( 'NONE',  ( 2.255458548909140770, -3.444374999999939568, 2.746210667320699184 ) ) ;
#247=EDGE_LOOP ( 'NONE', ( #5782, #13390 ) ) ;
#248=CARTESIAN_POINT ( 'NONE',  ( 3.211975673186791891, -5.553749999999917364, 0.6376497042497289991 ) ) ;
#250=CARTESIAN_POINT ( 'NONE',  ( -2.085189712146006347, 0.3281249999999837907, 3.904486635941227579 ) ) ;
#251=CARTESIAN_POINT ( 'NONE',  ( -4.010609860205056165, -1.452338562373114650, -1.217768749654296601 ) ) ;
#262=CARTESIAN_POINT ( 'NONE',  ( -2.390027884620886667, -4.640624999999809042, 2.914437415443186907 ) ) ;
#264=CARTESIAN_POINT ( 'NONE',  ( 3.447003937676299312, -4.936713562372625042, 1.426311973487309981 ) ) ;
#280=CARTESIAN_POINT ( 'NONE',  ( 1.342127543875233808, -3.772500000000060805, -3.243584335895733251 ) ) ;
#283=ORIENTED_EDGE ( 'NONE', *, *, #13080, .F. ) ;
#285=AXIS2_PLACEMENT_3D ( 'NONE', #3423, #3496, #1409 ) ;
#286=CARTESIAN_POINT ( 'NONE',  ( -0.9158341974770886074, -5.184319124889475994, -3.470732244869258132 ) ) ;
#293=CIRCLE ( 'NONE', #12448, 3.250000000000016431 ) ;
#304=CARTESIAN_POINT ( 'NONE',  ( -1.090659875871078599, -1.881874999999897824, -3.598793876473114661 ) ) ;
#306=CARTESIAN_POINT ( 'NONE',  ( 3.389018004338130385, -4.078125000000095035, -1.813062472674689340 ) ) ;
#307=CARTESIAN_POINT ( 'NONE',  ( 3.637955631634659959, -5.499999999999999112, 4.455210719721457493E-16 ) ) ;
#312=AXIS2_PLACEMENT_3D ( 'NONE', #12956, #1156, #3249 ) ;
#315=AXIS2_PLACEMENT_3D ( 'NONE', #4207, #7855, #6470 ) ;
#323=ORIENTED_EDGE ( 'NONE', *, *, #3996, .F. ) ;
#325=CARTESIAN_POINT ( 'NONE',  ( -1.792750223658622799, -5.928749999999893383, -2.680858111629535578 ) ) ;
#328=CARTESIAN_POINT ( 'NONE',  ( 4.251316196654235213, -0.9992135623729603289, -0.001534204912023576835 ) ) ;
#334=DIRECTION ( 'NONE',  ( 1.000000000000000000, 0.000000000000000000, -6.982962677686266711E-15 ) ) ;
#346=EDGE_CURVE ( 'NONE', #2409, #13047, #3617, .T. ) ;
#348=( LENGTH_UNIT ( ) NAMED_UNIT ( * ) SI_UNIT ( .MILLI., .METRE. ) );
#349=CARTESIAN_POINT ( 'NONE',  ( 2.515861257320511246, -3.140624999999957367, -3.067863912704874796 ) ) ;
#350=ORIENTED_EDGE ( 'NONE', *, *, #4892, .F. ) ;
#351=CARTESIAN_POINT ( 'NONE',  ( -0.3627434553294616171, -5.264838562373213904, -3.669149073604559774 ) ) ;
#352=CARTESIAN_POINT ( 'NONE',  ( 3.852585042300790352, -0.6162500000000914469, -0.7652758215885018256 ) ) ;
#369=CARTESIAN_POINT ( 'NONE',  ( 3.647531283552059467, -2.600625000000050591, -0.3606074429803771131 ) ) ;
#373=CARTESIAN_POINT ( 'NONE',  ( 2.801881283053006655, -5.106938005630682120, -2.401640922905785125 ) ) ;
#376=AXIS2_PLACEMENT_3D ( 'NONE', #13204, #2563, #14504 ) ;
#380=CARTESIAN_POINT ( 'NONE',  ( 3.173335668876534399, -5.499999999999995559, 4.202682741317042909E-16 ) ) ;
#394=CARTESIAN_POINT ( 'NONE',  ( -2.084927739720960016, -1.928749999999817888, -3.122072247380865306 ) ) ;
#396=CARTESIAN_POINT ( 'NONE',  ( -2.497846391779839248, -3.359374999999932943, -3.045264817802638468 ) ) ;
#400=DIRECTION ( 'NONE',  ( 9.422394424380278809E-16, -1.000000000000000000, 0.000000000000000000 ) ) ;
#413=CARTESIAN_POINT ( 'NONE',  ( -2.348309169242666083, -5.210000000000155396, 2.347120911809276400 ) ) ;
#417=CARTESIAN_POINT ( 'NONE',  ( -2.348309169242665639, -5.210000000000155396, 2.347120911809276400 ) ) ;
#426=ORIENTED_EDGE ( 'NONE', *, *, #11897, .F. ) ;
#433=( NAMED_UNIT ( * ) PLANE_ANGLE_UNIT ( ) SI_UNIT ( $, .RADIAN. ) );
#434=CARTESIAN_POINT ( 'NONE',  ( 3.171456684173084906, -2.109375000000075051, -2.604672169174167884 ) ) ;
#442=MANIFOLD_SOLID_BREP ( 'Revolve3', #2613 ) ;
#450=SHAPE_REPRESENTATION_RELATIONSHIP ( 'NONE' , 'NONE' ,  #4448, #5164 ) ;
#454=CARTESIAN_POINT ( 'NONE',  ( -3.093239089446946810, -2.178749999999916476, 2.068481483294872358 ) ) ;
#456=ADVANCED_FACE ( 'NONE', ( #7724 ), #9806, .T. ) ;
#458=CARTESIAN_POINT ( 'NONE',  ( -2.941250829588631710, -5.234749468677339479, -1.940783535936075221 ) ) ;
#472=AXIS2_PLACEMENT_3D ( 'NONE', #3391, #12861, #2220 ) ;
#474=CARTESIAN_POINT ( 'NONE',  ( 2.605880849243368491, -2.459999999999848086, 2.603962797083386072 ) ) ;
#476=CARTESIAN_POINT ( 'NONE',  ( -0.3822054598150002591, -3.734374999999974243, 3.870204888229129114 ) ) ;
#489=CARTESIAN_POINT ( 'NONE',  ( -3.090028468548658314, -5.022500000000056808, -1.280849571915205987 ) ) ;
#492=CARTESIAN_POINT ( 'NONE',  ( -3.090028468548657425, -5.022500000000056808, -1.280849571915205765 ) ) ;
#502=VERTEX_POINT ( 'NONE', #4752 ) ;
#505=CARTESIAN_POINT ( 'NONE',  ( -3.121978066431621901, -2.609375000000007550, 2.560763078121147451 ) ) ;
#511=CARTESIAN_POINT ( 'NONE',  ( 0.4577183133098803314, 2.374744442174770764, 4.500000000000000000 ) ) ;
#514=EDGE_CURVE ( 'NONE', #4411, #9101, #13291, .T. ) ;
#517=EDGE_LOOP ( 'NONE', ( #6569, #13358, #11148, #3402 ) ) ;
#518=EDGE_CURVE ( 'NONE', #11322, #8008, #639, .T. ) ;
#522=CARTESIAN_POINT ( 'NONE',  ( -3.566427039428708756, -2.131875000000089670, 1.083295335393480441 ) ) ;
#532=ADVANCED_FACE ( 'NONE', ( #2423 ), #6094, .F. ) ;
#543=AXIS2_PLACEMENT_3D ( 'NONE', #12547, #5252, #11219 ) ;
#545=CARTESIAN_POINT ( 'NONE',  ( -1.508667427112231785, -3.312499999999990674, -3.644952880303303555 ) ) ;
#549=CARTESIAN_POINT ( 'NONE',  ( -3.440513747128907784, 2.288586792248386903, -3.040855385833559854 ) ) ;
#550=CARTESIAN_POINT ( 'NONE',  ( -4.010754789764311212, -1.453125000000109912, -1.215065766439024975 ) ) ;
#551=CARTESIAN_POINT ( 'NONE',  ( -5.196152422706630247, 0.1227504548087275521, -7.569115911492098221E-16 ) ) ;
#564=CARTESIAN_POINT ( 'NONE',  ( -2.598582712860348032, -0.4995676945082659359, 3.267044563363100895 ) ) ;
#567=CARTESIAN_POINT ( 'NONE',  ( -3.336666538900096679, -5.084999999999988418, 0.001247370357366475637 ) ) ;
#572=CARTESIAN_POINT ( 'NONE',  ( -3.978302601493375334, -2.468750000000105693, -0.7924256976418916354 ) ) ;
#574=AXIS2_PLACEMENT_3D ( 'NONE', #12587, #10085, #7779 ) ;
#590=CARTESIAN_POINT ( 'NONE',  ( -2.084927739720960460, -1.928749999999817888, -3.122072247380865306 ) ) ;
#597=CARTESIAN_POINT ( 'NONE',  ( 3.464101615137753054, 8.706078090612013285E-15, -3.000000000000000444 ) ) ;
#604=ORIENTED_EDGE ( 'NONE', *, *, #11290, .F. ) ;
#613=CARTESIAN_POINT ( 'NONE',  ( 3.589928677163299220, -5.999213562373140185, 0.0009248216214229900388 ) ) ;
#614=CARTESIAN_POINT ( 'NONE',  ( -2.355664480073890399, -2.225624999999979092, 2.872538697791624518 ) ) ;
#617=CARTESIAN_POINT ( 'NONE',  ( 1.826535687659961660, -3.828124999999970246, 3.419360526609917628 ) ) ;
#623=CARTESIAN_POINT ( 'NONE',  ( -1.612261674935887568, -1.312500000000171863, -3.888369303904286589 ) ) ;
#633=ORIENTED_EDGE ( 'NONE', *, *, #10187, .T. ) ;
#637=CARTESIAN_POINT ( 'NONE',  ( -2.589953986283601850, -4.975625000000236220, -2.126619835350766152 ) ) ;
#639=CIRCLE ( 'NONE', #15241, 4.362044368365340041 ) ;
#641=CARTESIAN_POINT ( 'NONE',  ( -3.031088913245534311, 0.04639863247562460435, -3.750000000000000444 ) ) ;
#646=B_SPLINE_CURVE_WITH_KNOTS ( 'NONE', 3,
 ( #7069, #3331, #8063, #12799, #4573, #9298, #8145, #6150, #8215, #13039, #13186, #2316 ),
 .UNSPECIFIED., .F., .F.,
 ( 4, 2, 2, 2, 2, 4 ),
 ( 2.544323688695373385E-07, 0.001342108318545691186, 0.002013035261634102662, 0.002683962204722513054, 0.004025816090899333836, 0.005367669977076155487 ),
 .UNSPECIFIED. ) ;
#652=ORIENTED_EDGE ( 'NONE', *, *, #1449, .F. ) ;
#654=CARTESIAN_POINT ( 'NONE',  ( 2.924917369268297485, -1.874999999999847455, 2.922799279172734632 ) ) ;
#663=CARTESIAN_POINT ( 'NONE',  ( -1.120937138200071015, 2.242130364950076782, 4.499999999999999112 ) ) ;
#664=CARTESIAN_POINT ( 'NONE',  ( -2.598076211353315568, 0.1227504548087345604, 4.500000000000000888 ) ) ;
#670=CARTESIAN_POINT ( 'NONE',  ( -3.204583014436231281, -1.178749999999988640, 2.140022251743640691 ) ) ;
#673=EDGE_CURVE ( 'NONE', #10438, #8132, #3367, .T. ) ;
#691=CARTESIAN_POINT ( 'NONE',  ( -0.001316410337383604624, -6.249213562373078013, -3.556817731968370033 ) ) ;
#692=CARTESIAN_POINT ( 'NONE',  ( -0.3768771888557862493, -1.319375000000004405, 3.816279424444235069 ) ) ;
#695=CARTESIAN_POINT ( 'NONE',  ( 2.924917369268297485, -1.874999999999847455, 2.922799279172734632 ) ) ;
#696=DIRECTION ( 'NONE',  ( -9.422394424380278809E-16, 1.000000000000000000, -0.000000000000000000 ) ) ;
#699=CARTESIAN_POINT ( 'NONE',  ( -5.196152422706634688, 1.678847577293359539, -8.911270275552416508E-16 ) ) ;
#700=CARTESIAN_POINT ( 'NONE',  ( -3.324804228637022074, -0.6093749999999287237, 2.730601746129839746 ) ) ;
#702=DIRECTION ( 'NONE',  ( -2.551930889570659960E-15, 1.000000000000000000, 0.000000000000000000 ) ) ;
#708=AXIS2_PLACEMENT_3D ( 'NONE', #11617, #5583, #12482 ) ;
#714=CARTESIAN_POINT ( 'NONE',  ( -0.6461339251375918247, -5.303750000000252207, 3.244047683681893446 ) ) ;
#720=CARTESIAN_POINT ( 'NONE',  ( -2.226241924188425703, -0.4995676945082649367, 3.513072387502060412 ) ) ;
#722=DIRECTION ( 'NONE',  ( -1.000000000000000000, 0.000000000000000000, 0.000000000000000000 ) ) ;
#724=FACE_OUTER_BOUND ( 'NONE', #247, .T. ) ;
#729=CARTESIAN_POINT ( 'NONE',  ( -1.243836315904764955, -0.7031249999999807931, 4.105705763534058583 ) ) ;
#731=CARTESIAN_POINT ( 'NONE',  ( -3.614955235551140511, -3.561713562373173936, 1.496253015928757701 ) ) ;
#741=CARTESIAN_POINT ( 'NONE',  ( -2.629016928070554204, -2.210000000000078568, 2.627652665972901147 ) ) ;
#754=CARTESIAN_POINT ( 'NONE',  ( -1.562933739280453427, -5.256875000000181153, 2.922265072135110664 ) ) ;
#760=CARTESIAN_POINT ( 'NONE',  ( 1.112125432426118499, -1.381875000000161391, 3.661359949639011901 ) ) ;
#762=CARTESIAN_POINT ( 'NONE',  ( 3.171456684173084906, -2.109375000000075051, -2.604672169174167884 ) ) ;
#767=CARTESIAN_POINT ( 'NONE',  ( 1.916065064279496746E-15, 7.362499999999997158, 0.000000000000000000 ) ) ;
#775=AXIS2_PLACEMENT_3D ( 'NONE', #10023, #10964, #5075 ) ;
#778=PRODUCT_DEFINITION_CONTEXT ( 'detailed design', #1975, 'design' ) ;
#781=CARTESIAN_POINT ( 'NONE',  ( 0.001278483876788636883, -4.335000000000164277, 3.435880605283331501 ) ) ;
#782=AXIS2_PLACEMENT_3D ( 'NONE', #3127, #7999, #7863 ) ;
#791=AXIS2_PLACEMENT_3D ( 'NONE', #4393, #3219, #6883 ) ;
#797=LINE ( 'NONE', #13911, #5495 ) ;
#800=CARTESIAN_POINT ( 'NONE',  ( -4.293856390582560856, -0.5156249999999756861, 0.4244695705039617240 ) ) ;
#803=CARTESIAN_POINT ( 'NONE',  ( -4.035363762266634957, -2.483588562372986086, -0.3985244866878402958 ) ) ;
#804=DIRECTION ( 'NONE',  ( 1.747085166004344019E-15, -1.000000000000000000, 0.000000000000000000 ) ) ;
#819=CARTESIAN_POINT ( 'NONE',  ( 2.349903878712679806, -5.140624999999672262, -2.861852458627701434 ) ) ;
#821=CARTESIAN_POINT ( 'NONE',  ( 2.100337907687909400, -1.741249999999995968, -3.141606438102765075 ) ) ;
#837=CARTESIAN_POINT ( 'NONE',  ( 0.9968050443165104024, -4.381875000000003517, 3.281628308787421844 ) ) ;
#839=ORIENTED_EDGE ( 'NONE', *, *, #12386, .T. ) ;
#841=CARTESIAN_POINT ( 'NONE',  ( 0.3497462729172694518, -6.233588562373080677, -3.541697392899130659 ) ) ;
#842=CARTESIAN_POINT ( 'NONE',  ( 0.7624512442115692901, -0.8037500000000172840, -3.827857439461599398 ) ) ;
#844=CARTESIAN_POINT ( 'NONE',  ( -0.001482159116125898214, -2.249999999999994227, -4.085353063378265759 ) ) ;
#845=AXIS2_PLACEMENT_3D ( 'NONE', #10999, #1460, #3868 ) ;
#849=CARTESIAN_POINT ( 'NONE',  ( -4.296274425956841725, -0.5002988223950231017, 0.02453012155904704325 ) ) ;
#850=CARTESIAN_POINT ( 'NONE',  ( -2.335396930795095471, -1.343749999999818368, -3.497180482087419051 ) ) ;
#867=CARTESIAN_POINT ( 'NONE',  ( -3.252405029756590515, -0.4995676945082676568, 2.664931962243846097 ) ) ;
#878=CARTESIAN_POINT ( 'NONE',  ( 0.001121683909886545937, -1.249999999999918066, -4.217678074926116238 ) ) ;
#880=CARTESIAN_POINT ( 'NONE',  ( 0.001080389160871208457, -2.249213562373011843, -4.085999009053598918 ) ) ;
#888=EDGE_CURVE ( 'NONE', #1688, #9382, #4871, .T. ) ;
#896=CARTESIAN_POINT ( 'NONE',  ( 2.372013019084901586, -4.859374999999952927, 2.891838320553053343 ) ) ;
#899=ADVANCED_FACE ( 'NONE', ( #13961 ), #12648, .F. ) ;
#900=CARTESIAN_POINT ( 'NONE',  ( 2.822884439542639790, -2.694375000000075460, -2.318423337397389261 ) ) ;
#914=TOROIDAL_SURFACE ( 'NONE', #14545, 2.931404194366992400, 0.5000000000000000000 ) ;
#916=CARTESIAN_POINT ( 'NONE',  ( -0.6836773592642515496, -3.866249999999994635, -3.430425219284938265 ) ) ;
#919=EDGE_LOOP ( 'NONE', ( #10109, #1775, #5406, #6735 ) ) ;
#920=CARTESIAN_POINT ( 'NONE',  ( -2.836763133589473629, -5.389838562373330255, -2.329300430828157076 ) ) ;
#921=CARTESIAN_POINT ( 'NONE',  ( -3.916933349122106112, -0.1162499999999876271, 0.7806084585172713419 ) ) ;
#922=CARTESIAN_POINT ( 'NONE',  ( -3.119281932368198618, -5.304704016482149953, 1.429041148738060985 ) ) ;
#923=CARTESIAN_POINT ( 'NONE',  ( 0.4017167453136591404, -2.234374999999921396, -4.067671435978028605 ) ) ;
#939=CARTESIAN_POINT ( 'NONE',  ( 0.0008557816480155369665, -4.835000000000089670, -3.369777484087370212 ) ) ;
#944=B_SPLINE_CURVE_WITH_KNOTS ( 'NONE', 3,
 ( #11651, #15208, #10718, #83 ),
 .UNSPECIFIED., .F., .F.,
 ( 4, 4 ),
 ( 0.002598307151460989371, 0.005196383362814305240 ),
 .UNSPECIFIED. ) ;
#953=VERTEX_POINT ( 'NONE', #6361 ) ;
#956=CARTESIAN_POINT ( 'NONE',  ( 0.4056240317150583419, -1.765625000000045741, 4.129595427369183724 ) ) ;
#958=CARTESIAN_POINT ( 'NONE',  ( -0.3927583221446535044, -2.733588562373027830, 4.002660525033727268 ) ) ;
#972=CARTESIAN_POINT ( 'NONE',  ( 3.852585042300790796, -0.6162500000000914469, -0.7652758215885019366 ) ) ;
#974=CARTESIAN_POINT ( 'NONE',  ( 3.244093391032126572, -2.506875000000020837, 1.732468392772068544 ) ) ;
#977=CARTESIAN_POINT ( 'NONE',  ( 3.676486008612421585, -0.4995676945082496712, 1.453030271339659008 ) ) ;
#987=CARTESIAN_POINT ( 'NONE',  ( 1.592243150387700146, -4.756875000000070131, -2.981552405995577804 ) ) ;
#992=CARTESIAN_POINT ( 'NONE',  ( 3.431607731776029180, -5.061713562373087782, -1.420375347272441857 ) ) ;
#993=EDGE_CURVE ( 'NONE', #8371, #10438, #9314, .T. ) ;
#994=CARTESIAN_POINT ( 'NONE',  ( 3.049996619588533520, -0.4756250000000030176, 2.504408566260877489 ) ) ;
#995=CARTESIAN_POINT ( 'NONE',  ( -3.582436959730881831, -2.421875000000131450, -1.916069189016956331 ) ) ;
#1001=DIRECTION ( 'NONE',  ( -1.669238443041288662E-16, -4.259781144855898747E-31, -1.000000000000000000 ) ) ;
#1002=CARTESIAN_POINT ( 'NONE',  ( 3.388605160257775140, -4.569374999999831211, 0.3324735777646720680 ) ) ;
#1012=CARTESIAN_POINT ( 'NONE',  ( 3.136514378097080780, -4.647499999999995524, -1.298252083346796759 ) ) ;
#1028=ORIENTED_EDGE ( 'NONE', *, *, #1342, .F. ) ;
#1030=CARTESIAN_POINT ( 'NONE',  ( -3.998008487304611336, -1.546875000000091038, 1.214361949261595131 ) ) ;
#1032=CARTESIAN_POINT ( 'NONE',  ( 3.914479021157896810, -2.967963562373050923, 0.7771573004458622869 ) ) ;
#1041=CARTESIAN_POINT ( 'NONE',  ( 3.530157234965975555, -5.226201182446649440, -2.246195850846843811E-13 ) ) ;
#1045=CARTESIAN_POINT ( 'NONE',  ( -3.637955631634660403, -5.500000000000000000, 0.000000000000000000 ) ) ;
#1049=CARTESIAN_POINT ( 'NONE',  ( 1.394838545734166990, -2.772499999999996856, -3.364978284447634582 ) ) ;
#1051=DIRECTION ( 'NONE',  ( -1.747085166004344019E-15, 1.000000000000000000, -0.000000000000000000 ) ) ;
#1061=ORIENTED_EDGE ( 'NONE', *, *, #4996, .F. ) ;
#1062=CARTESIAN_POINT ( 'NONE',  ( -3.196762997434542175, -4.147500000000007958, 1.325534829466322062 ) ) ;
#1064=EDGE_LOOP ( 'NONE', ( #13321, #2642, #1345, #3553 ) ) ;
#1068=CARTESIAN_POINT ( 'NONE',  ( -0.3692575584143804046, -4.733588562373068243, 3.739163940647424855 ) ) ;
#1077=DIRECTION ( 'NONE',  ( -9.422394424380278809E-16, 1.000000000000000000, -0.000000000000000000 ) ) ;
#1082=CARTESIAN_POINT ( 'NONE',  ( 1.682902201845278611, -5.420849775684215999, 2.811263474311217259 ) ) ;
#1089=ORIENTED_EDGE ( 'NONE', *, *, #7043, .T. ) ;
#1091=EDGE_CURVE ( 'NONE', #2409, #160, #8338, .T. ) ;
#1093=CARTESIAN_POINT ( 'NONE',  ( -1.685726645313963434, -3.256874999999974651, 3.156579729352138486 ) ) ;
#1098=CARTESIAN_POINT ( 'NONE',  ( 3.291891004236185747, -4.921874999999971578, 1.757997479805845975 ) ) ;
#1101=FACE_OUTER_BOUND ( 'NONE', #6719, .T. ) ;
#1110=CARTESIAN_POINT ( 'NONE',  ( -1.629699455448989389E-14, 8.699999999999999289, 5.655858585055787181E-29 ) ) ;
#1115=CARTESIAN_POINT ( 'NONE',  ( -3.565751477134541769, -2.577338562373002961, 1.904724266850964520 ) ) ;
#1129=CARTESIAN_POINT ( 'NONE',  ( 2.507317702870420106, -0.4443749999999629940, 3.052905756198935894 ) ) ;
#1131=CONICAL_SURFACE ( 'NONE', #11533, 3.637955631634646192, 0.1308996938995775905 ) ;
#1132=CARTESIAN_POINT ( 'NONE',  ( -2.557519727433407386, -2.960000000000007958, -2.558839988362045403 ) ) ;
#1147=CARTESIAN_POINT ( 'NONE',  ( 3.136514378097081224, -4.647499999999995524, -1.298252083346754793 ) ) ;
#1149=AXIS2_PLACEMENT_3D ( 'NONE', #2170, #13884, #3253 ) ;
#1153=CARTESIAN_POINT ( 'NONE',  ( -1.797749598780369329, -4.327338562373237885, -3.360391230360182835 ) ) ;
#1156=DIRECTION ( 'NONE',  ( 9.422394424380274864E-16, -1.000000000000000000, 0.000000000000000000 ) ) ;
#1159=AXIS2_PLACEMENT_3D ( 'NONE', #3987, #8718, #6116 ) ;
#1162=CARTESIAN_POINT ( 'NONE',  ( -2.669536895096369378, -4.194375000000057696, 2.192493760422927984 ) ) ;
#1171=CARTESIAN_POINT ( 'NONE',  ( 3.389189273868536745, -3.538124999999807674, 1.026728768593236030 ) ) ;
#1179=CARTESIAN_POINT ( 'NONE',  ( -4.296789059413591794, -0.4989263220255817921, -0.007758693162678284572 ) ) ;
#1187=ORIENTED_EDGE ( 'NONE', *, *, #9491, .T. ) ;
#1191=CARTESIAN_POINT ( 'NONE',  ( 2.445585954864915479, 0.1562500000001365852, 3.662202016184997522 ) ) ;
#1193=CARTESIAN_POINT ( 'NONE',  ( -3.981650243116422683, -0.5617135623731067673, 1.648008353199287290 ) ) ;
#1206=CARTESIAN_POINT ( 'NONE',  ( -4.500000000000006217, 2.374999999999988454, 0.000000000000000000 ) ) ;
#1207=CARTESIAN_POINT ( 'NONE',  ( 2.991150664073139342, -3.890625000000195399, 2.452944570972435567 ) ) ;
#1219=CARTESIAN_POINT ( 'NONE',  ( -1.629699455448989389E-14, 8.699999999999999289, 5.655858585055787181E-29 ) ) ;
#1222=CARTESIAN_POINT ( 'NONE',  ( 1.740706783794652823, -2.413124999999917808, 3.253752085064650412 ) ) ;
#1227=CARTESIAN_POINT ( 'NONE',  ( -1.090569219518439548, -4.702338562373102882, 3.599880871716213626 ) ) ;
#1234=CARTESIAN_POINT ( 'NONE',  ( 0.001278483876788636883, -4.335000000000164277, 3.435880605283331501 ) ) ;
#1243=CARTESIAN_POINT ( 'NONE',  ( 2.928286698324767290, -3.678750000000110987, -1.958188979435658839 ) ) ;
#1245=CARTESIAN_POINT ( 'NONE',  ( 3.163831456873871684, -5.086585887928589678, -1.913743399047732607 ) ) ;
#1259=CARTESIAN_POINT ( 'NONE',  ( 4.187874307737824431, -0.04687499999988285065, -1.272022143297006025 ) ) ;
#1260=ORIENTED_EDGE ( 'NONE', *, *, #8372, .F. ) ;
#1262=CARTESIAN_POINT ( 'NONE',  ( -4.296821574387140963, -0.4992135623730943328, -3.600545362394707632E-13 ) ) ;
#1263=AXIS2_PLACEMENT_3D ( 'NONE', #14836, #6645, #722 ) ;
#1271=LINE ( 'NONE', #14150, #5141 ) ;
#1278=CARTESIAN_POINT ( 'NONE',  ( -1.775679308629948050, -4.671875000000182077, 3.319983975552966537 ) ) ;
#1282=CARTESIAN_POINT ( 'NONE',  ( 0.7624512442115692901, -0.8037500000000172840, -3.827857439461599398 ) ) ;
#1287=EDGE_CURVE ( 'NONE', #6270, #8008, #30, .T. ) ;
#1296=ORIENTED_EDGE ( 'NONE', *, *, #8726, .F. ) ;
#1299=CARTESIAN_POINT ( 'NONE',  ( 1.363531154075422469, -3.397500000000037712, 3.288412936073061399 ) ) ;
#1301=EDGE_LOOP ( 'NONE', ( #14048, #2174, #14673, #6484 ) ) ;
#1306=CARTESIAN_POINT ( 'NONE',  ( -4.330127018922191873, -1.133557105241920558E-14, -1.499999999999999334 ) ) ;
#1308=CARTESIAN_POINT ( 'NONE',  ( 7.511572993685698521E-16, 1.916901515185129432E-30, 4.500000000000000888 ) ) ;
#1311=CARTESIAN_POINT ( 'NONE',  ( -0.6956252696767697419, -3.303750000000123421, 3.503916970779588969 ) ) ;
#1314=DIRECTION ( 'NONE',  ( 1.000000000000000000, 0.000000000000000000, -6.982962677686266711E-15 ) ) ;
#1321=CARTESIAN_POINT ( 'NONE',  ( 3.273328345814555007, -3.522500000000126974, 1.356842221127619874 ) ) ;
#1331=CARTESIAN_POINT ( 'NONE',  ( -3.081487911019577365E-30, 0.000000000000000000, 0.000000000000000000 ) ) ;
#1342=EDGE_CURVE ( 'NONE', #6229, #10656, #6534, .T. ) ;
#1343=AXIS2_PLACEMENT_3D ( 'NONE', #10603, #3548, #2382 ) ;
#1344=CARTESIAN_POINT ( 'NONE',  ( -4.103321639749550442, 0.4374999999999862332, 1.698361598734861477 ) ) ;
#1345=ORIENTED_EDGE ( 'NONE', *, *, #5839, .T. ) ;
#1346=CARTESIAN_POINT ( 'NONE',  ( 1.240811975207549933, -0.7960885623730461491, 4.094338395617355353 ) ) ;
#1351=AXIS2_PLACEMENT_3D ( 'NONE', #14097, #4713, #8040 ) ;
#1357=DIRECTION ( 'NONE',  ( -1.747085166004344019E-15, 1.000000000000000000, -0.000000000000000000 ) ) ;
#1360=CARTESIAN_POINT ( 'NONE',  ( 3.783699349552338997, -3.968750000000262013, 0.7536532579988950431 ) ) ;
#1372=DIRECTION ( 'NONE',  ( -1.000000000000000000, -1.682335022489801357E-15, 0.000000000000000000 ) ) ;
#1373=EDGE_CURVE ( 'NONE', #9101, #11935, #1271, .T. ) ;
#1376=ORIENTED_EDGE ( 'NONE', *, *, #9420, .T. ) ;
#1380=VERTEX_POINT ( 'NONE', #4463 ) ;
#1381=ADVANCED_FACE ( 'NONE', ( #6882 ), #3526, .F. ) ;
#1384=CARTESIAN_POINT ( 'NONE',  ( 2.024885806073562389, -2.741249999999974207, -3.032875982375833335 ) ) ;
#1386=VERTEX_POINT ( 'NONE', #1589 ) ;
#1399=CARTESIAN_POINT ( 'NONE',  ( 3.109021928378527200, -3.663124999999927578, -1.660781358202984448 ) ) ;
#1409=DIRECTION ( 'NONE',  ( 1.000000000000000000, 0.000000000000000000, 0.000000000000000000 ) ) ;
#1410=CARTESIAN_POINT ( 'NONE',  ( 0.3573659033054957801, -2.819374999999921805, -3.618812876704415427 ) ) ;
#1416=LINE ( 'NONE', #9, #5657 ) ;
#1419=DIRECTION ( 'NONE',  ( 2.551930889570659960E-15, -1.000000000000000000, -0.000000000000000000 ) ) ;
#1429=CARTESIAN_POINT ( 'NONE',  ( -3.700822939793764643, -1.421088562373072239, -1.976411301434599865 ) ) ;
#1430=DIRECTION ( 'NONE',  ( -1.747085166004344019E-15, 1.000000000000000000, -0.000000000000000000 ) ) ;
#1442=CARTESIAN_POINT ( 'NONE',  ( -3.466918327573330849, -3.421874999999993339, -1.851480974780293387 ) ) ;
#1446=ADVANCED_FACE ( 'NONE', ( #14607 ), #11315, .T. ) ;
#1447=CARTESIAN_POINT ( 'NONE',  ( -1.967370292840699531, -5.340790585608573338, 2.765304479937676696 ) ) ;
#1449=EDGE_CURVE ( 'NONE', #7901, #10851, #6635, .T. ) ;
#1450=DIRECTION ( 'NONE',  ( -2.551930889570660354E-15, 1.000000000000000000, 0.000000000000000000 ) ) ;
#1460=DIRECTION ( 'NONE',  ( -6.860497997771531562E-15, -6.464231808267455010E-30, -1.000000000000000000 ) ) ;
#1461=CARTESIAN_POINT ( 'NONE',  ( -0.001340710925747427232, -2.834999999999994635, -3.634308738048292131 ) ) ;
#1486=CARTESIAN_POINT ( 'NONE',  ( -1.859859099471618649, -3.328125000000058620, -3.476502332403788476 ) ) ;
#1490=ORIENTED_EDGE ( 'NONE', *, *, #6678, .F. ) ;
#1501=CARTESIAN_POINT ( 'NONE',  ( -2.968563080203957760, -6.022500000000311715, -1.228311040920463615 ) ) ;
#1503=CARTESIAN_POINT ( 'NONE',  ( 3.523678346781135229, -1.092963562373023167, -2.356287093288357060 ) ) ;
#1506=DIRECTION ( 'NONE',  ( -6.982962677686266711E-15, -6.579622859988665673E-30, -1.000000000000000000 ) ) ;
#1513=CARTESIAN_POINT ( 'NONE',  ( -3.711107677420292905, -4.531250000000010658, 0.7371803430742600582 ) ) ;
#1514=ORIENTED_EDGE ( 'NONE', *, *, #993, .T. ) ;
#1515=CARTESIAN_POINT ( 'NONE',  ( 2.057266006166119432, -5.155463562373004294, -3.077188522048795338 ) ) ;
#1517=CARTESIAN_POINT ( 'NONE',  ( -0.7612222386588485268, -0.8662499999999671019, -3.819631723157196568 ) ) ;
#1523=CARTESIAN_POINT ( 'NONE',  ( 3.500468167958952659, -5.241858618441043838, 0.2938655770740091211 ) ) ;
#1532=CARTESIAN_POINT ( 'NONE',  ( 2.605880849243188191, -2.459999999999848086, 2.603962797083296365 ) ) ;
#1542=CARTESIAN_POINT ( 'NONE',  ( -1.552469261541196355, -0.4995676945082632159, -3.889349939136176548 ) ) ;
#1555=CARTESIAN_POINT ( 'NONE',  ( 3.059130242547580814, -2.491250000000117204, 2.045191655759024396 ) ) ;
#1557=CARTESIAN_POINT ( 'NONE',  ( -1.106373576938931125, -4.296874999999863221, -3.650653549769442119 ) ) ;
#1575=CARTESIAN_POINT ( 'NONE',  ( -0.001216256839607805784, -5.834999999999983977, -3.237452472516330282 ) ) ;
#1576=EDGE_CURVE ( 'NONE', #6229, #7479, #5434, .T. ) ;
#1580=CARTESIAN_POINT ( 'NONE',  ( -2.933994605034232706, -5.163125000000027498, 1.567297863280144865 ) ) ;
#1589=CARTESIAN_POINT ( 'NONE',  ( 1.682902201845278611, -5.420849775684215999, 2.811263474311217259 ) ) ;
#1595=CARTESIAN_POINT ( 'NONE',  ( -0.7951559085591690668, -2.281249999999988010, -4.003048974988245412 ) ) ;
#1597=CARTESIAN_POINT ( 'NONE',  ( -3.903921151840624493, -3.483588562373245878, -0.3830646067732271787 ) ) ;
#1609=( NAMED_UNIT ( * ) PLANE_ANGLE_UNIT ( ) SI_UNIT ( $, .RADIAN. ) );
#1612=CARTESIAN_POINT ( 'NONE',  ( 2.674095735623996273, -1.709999999999972209, -2.676057788957755701 ) ) ;
#1616=CARTESIAN_POINT ( 'NONE',  ( -0.7374914331583092286, -5.180749959738387922, -3.517645758868249040 ) ) ;
#1636=CARTESIAN_POINT ( 'NONE',  ( 0.7342756466162075890, -1.803750000000060361, -3.698544502508174681 ) ) ;
#1637=FACE_OUTER_BOUND ( 'NONE', #5202, .T. ) ;
#1638=CARTESIAN_POINT ( 'NONE',  ( 1.127871658241229147, -3.796875000000003553, 3.713209756639876069 ) ) ;
#1655=CARTESIAN_POINT ( 'NONE',  ( 2.085982869228584224, -5.444374999999953779, 2.543086608318696928 ) ) ;
#1659=CARTESIAN_POINT ( 'NONE',  ( 1.242853247313944420, -5.772499999999809006, -2.998378529913433344 ) ) ;
#1674=FILL_AREA_STYLE_COLOUR ( '', #2124 ) ;
#1675=ADVANCED_FACE ( 'NONE', ( #724, #8877 ), #7720, .T. ) ;
#1676=CARTESIAN_POINT ( 'NONE',  ( 3.820852842225918700, -2.953124999999806821, 1.157524667501716786 ) ) ;
#1688=VERTEX_POINT ( 'NONE', #3279 ) ;
#1691=CARTESIAN_POINT ( 'NONE',  ( 0.7459506331255062461, -1.366249999999944897, 3.755271276440845796 ) ) ;
#1696=CIRCLE ( 'NONE', #4685, 4.500000000000000888 ) ;
#1700=ORIENTED_EDGE ( 'NONE', *, *, #2607, .T. ) ;
#1708=CARTESIAN_POINT ( 'NONE',  ( 3.783562653031121936, -1.569374999999871845, 0.3712484392075319217 ) ) ;
#1711=CARTESIAN_POINT ( 'NONE',  ( -1.491583768208377681, -3.687499999999984901, 3.598334897712680114 ) ) ;
#1725=CARTESIAN_POINT ( 'NONE',  ( 1.260313249030111438, -5.397499999999716636, 3.044840626206112955 ) ) ;
#1726=EDGE_CURVE ( 'NONE', #10851, #13125, #2192, .T. ) ;
#1732=CARTESIAN_POINT ( 'NONE',  ( -4.296274425956841725, -0.5002988223950231017, 0.02453012155904704325 ) ) ;
#1733=CARTESIAN_POINT ( 'NONE',  ( -1.864549691619314498, -4.928749999999819664, -2.792029179168366237 ) ) ;
#1734=ORIENTED_EDGE ( 'NONE', *, *, #13246, .T. ) ;
#1736=B_SPLINE_CURVE_WITH_KNOTS ( 'NONE', 3,
 ( #165, #3811, #1245, #4912, #10632, #13286, #11730, #8236, #10713, #1098, #6171, #10557, #2339, #8392, #12977, #7089, #11880, #13205, #2564, #7314, #13590, #7396, #8690, #10945, #4122, #1783, #12419, #2721, #7627, #6390, #13513, #11252, #11024, #8771, #13436, #11171, #1557, #7696, #8848, #2649, #2956, #3963, #6461, #5291, #2880, #306, #6537, #5055, #2798, #12348, #14736, #8920, #12267, #14809, #9770, #7549, #617, #1638, #5373, #10077, #476, #11103, #1711, #5211, #10002, #12186, #9924, #6312, #9852, #7468, #14657, #14505, #4196, #12118, #3891, #4042, #396, #1486, #545, #6238, #8617, #13364, #5142, #14583, #6913, #13736, #7844, #15034, #1863, #3327, #8060, #3182, #4349, #13658, #7910, #2163, #11633, #10144, #3108, #12578, #2086, #15104, #10452, #10223, #15183, #1940, #5520, #6757, #9073, #13879, #10379, #4570, #12641, #3028, #11328, #13813, #995, #2007, #5750, #13954, #11478, #14955, #7980, #844, #923, #6687, #5602, #11397, #10307, #762, #4423, #6620, #5684, #7771, #14876, #9142, #3248, #12502, #6838, #695, #11559, #4493, #5446, #9214, #4265, #12797, #13595, #5450, #7633, #9077, #13819, #8925, #10082, #4048, #13662, #7914, #2011, #550, #8852, #4126, #7849, #5526, #850, #623, #5606, #2961, #11259, #12508, #6465, #12646, #1788, #3033, #7775, #8997, #10149, #1868, #13742, #3112, #4201, #6763, #11483, #10311, #6626, #7700, #12423, #13518, #11175, #6541, #2884, #11333, #14813, #10227, #6692, #700, #11400, #14740, #14880, #5296, #8777, #5377 ),
 .UNSPECIFIED., .F., .F.,
 ( 4, 2, 2, 2, 2, 2, 2, 2, 2, 2, 2, 2, 2, 2, 2, 2, 2, 2, 2, 2, 2, 2, 2, 2, 2, 2, 2, 2, 2, 2, 2, 2, 2, 2, 2, 2, 2, 2, 2, 2, 2, 2, 2, 2, 2, 2, 2, 2, 2, 2, 2, 2, 2, 2, 2, 2, 2, 2, 2, 2, 2, 2, 2, 2, 2, 2, 2, 2, 2, 2, 2, 2, 2, 2, 2, 2, 2, 2, 2, 2, 2, 2, 2, 2, 2, 2, 2, 2, 2, 2, 2, 2, 2, 2, 2, 2, 2, 2, 2, 4 ),
 ( 0.06608205603566359720, 0.07031250000000000000, 0.07812500000000000000, 0.08593750000000000000, 0.09375000000000000000, 0.1015625000000000000, 0.1093750000000000000, 0.1171875000000000000, 0.1250000000000000000, 0.1328125000000000000, 0.1406250000000000000, 0.1484375000000000000, 0.1562500000000000000, 0.1640625000000000000, 0.1718750000000000000, 0.1796875000000000000, 0.1875000000000000000, 0.1953125000000000000, 0.2031250000000000000, 0.2109375000000000000, 0.2187500000000000000, 0.2265625000000000000, 0.2343750000000000000, 0.2421875000000000000, 0.2500000000000000000, 0.2578125000000000555, 0.2656250000000000000, 0.2734375000000000000, 0.2812500000000000000, 0.2890625000000000000, 0.2968750000000000000, 0.3046875000000000000, 0.3125000000000000000, 0.3203125000000000000, 0.3281250000000000000, 0.3359375000000000000, 0.3437500000000000000, 0.3515625000000000000, 0.3593750000000000000, 0.3671875000000000000, 0.3750000000000000000, 0.3828125000000000000, 0.3906250000000000000, 0.3984375000000000000, 0.4062499999999999445, 0.4140625000000000000, 0.4218750000000000000, 0.4296875000000000000, 0.4375000000000000000, 0.4453125000000000000, 0.4531250000000000000, 0.4609375000000000555, 0.4687500000000000000, 0.4765624999999999445, 0.4843750000000000000, 0.4921875000000000000, 0.5000000000000000000, 0.5078125000000000000, 0.5156250000000000000, 0.5234375000000000000, 0.5312500000000000000, 0.5390625000000000000, 0.5468750000000001110, 0.5546875000000000000, 0.5625000000000000000, 0.5703125000000000000, 0.5781250000000000000, 0.5859375000000000000, 0.5937500000000000000, 0.6015625000000000000, 0.6093750000000000000, 0.6171875000000000000, 0.6250000000000000000, 0.6328125000000000000, 0.6406250000000000000, 0.6484375000000000000, 0.6562500000000000000, 0.6640625000000000000, 0.6718750000000000000, 0.6796875000000000000, 0.6875000000000000000, 0.6953125000000000000, 0.7031250000000000000, 0.7109375000000000000, 0.7187500000000000000, 0.7265625000000000000, 0.7343750000000000000, 0.7421875000000001110, 0.7500000000000000000, 0.7578125000000000000, 0.7656250000000000000, 0.7734374999999998890, 0.7812500000000000000, 0.7890625000000000000, 0.7968750000000000000, 0.8046875000000000000, 0.8125000000000000000, 0.8203125000000000000, 0.8281250000000001110, 0.8331820081006554579 ),
 .UNSPECIFIED. ) ;
#1740=CARTESIAN_POINT ( 'NONE',  ( -1.169542390366794304, -2.703125000000013323, 3.851808151836873861 ) ) ;
#1745=CARTESIAN_POINT ( 'NONE',  ( -5.196152422706634688, 1.678847577293359539, -8.911270275552416508E-16 ) ) ;
#1747=CARTESIAN_POINT ( 'NONE',  ( -1.006616814747114065E-29, -2.568816543514387226E-44, 0.000000000000000000 ) ) ;
#1756=EDGE_LOOP ( 'NONE', ( #4563, #10317, #4029, #4206, #11393, #10915 ) ) ;
#1759=CARTESIAN_POINT ( 'NONE',  ( 3.518605591592443016, -1.522500000000036380, 1.455944046807712500 ) ) ;
#1763=CARTESIAN_POINT ( 'NONE',  ( 0.000000000000000000, 0.000000000000000000, 0.000000000000000000 ) ) ;
#1765=CARTESIAN_POINT ( 'NONE',  ( -1.764029795486899532, -5.202224379335410376, -3.099337613330489738 ) ) ;
#1775=ORIENTED_EDGE ( 'NONE', *, *, #888, .F. ) ;
#1781=CARTESIAN_POINT ( 'NONE',  ( -3.115386749435359093, -1.991250000000079678, -2.079980318098562098 ) ) ;
#1783=CARTESIAN_POINT ( 'NONE',  ( -3.618276846414829162, -4.546874999999968914, 1.099041561241040466 ) ) ;
#1788=CARTESIAN_POINT ( 'NONE',  ( 2.351042318464003689, -1.156249999999995559, -3.516557504029556913 ) ) ;
#1791=DIRECTION ( 'NONE',  ( 9.422394424380274864E-16, -1.000000000000000000, 0.000000000000000000 ) ) ;
#1793=DIRECTION ( 'NONE',  ( 0.4226182617407006625, -0.9063077870366492705, 0.000000000000000000 ) ) ;
#1799=CARTESIAN_POINT ( 'NONE',  ( -0.6299995022919476773, -5.866249999999999964, -3.171388681290751244 ) ) ;
#1802=CARTESIAN_POINT ( 'NONE',  ( -3.897114317029972685, -9.945166405816852549E-15, -2.249999999999999112 ) ) ;
#1807=CARTESIAN_POINT ( 'NONE',  ( 0.9968050443165101804, -4.381875000000003517, 3.281628308787421400 ) ) ;
#1814=CIRCLE ( 'NONE', #9238, 0.2500000000000000000 ) ;
#1815=CARTESIAN_POINT ( 'NONE',  ( 3.986138996993924266, -2.999999999999990674, -0.001451045610905104914 ) ) ;
#1826=CARTESIAN_POINT ( 'NONE',  ( 1.771711357477687043, 2.042612654300325570, 4.500000000000000000 ) ) ;
#1834=CARTESIAN_POINT ( 'NONE',  ( 1.096135970525343728, -1.788124999999989750, -3.610092524386872004 ) ) ;
#1857=CARTESIAN_POINT ( 'NONE',  ( -3.656031798353854168, -5.499213562373083342, 0.001347523837372742971 ) ) ;
#1858=EDGE_CURVE ( 'NONE', #11015, #9386, #12079, .T. ) ;
#1859=CARTESIAN_POINT ( 'NONE',  ( -3.224082633657694430, -0.9912500000000042943, -2.155484159616896989 ) ) ;
#1863=CARTESIAN_POINT ( 'NONE',  ( 3.506874188274308413, -3.078124999999926281, -1.873277435140577429 ) ) ;
#1868=CARTESIAN_POINT ( 'NONE',  ( 4.164680137118252468, -1.031249999999941602, -0.8299691317567963189 ) ) ;
#1881=CARTESIAN_POINT ( 'NONE',  ( 3.135427973343609231, -5.538124999999991971, 0.9519854854111799991 ) ) ;
#1888=CARTESIAN_POINT ( 'NONE',  ( 2.709010606882195304, -0.4995676945082524467, 2.903689985453846489 ) ) ;
#1899=CARTESIAN_POINT ( 'NONE',  ( 3.689984836354881281, -2.937500000000126565, 1.529580092797385715 ) ) ;
#1901=DIRECTION ( 'NONE',  ( 1.000000000000000000, 0.000000000000000000, 1.224646799147353207E-16 ) ) ;
#1908=DIRECTION ( 'NONE',  ( -1.224646799147353207E-16, -2.139562256385042123E-31, 1.000000000000000000 ) ) ;
#1914=CARTESIAN_POINT ( 'NONE',  ( -3.657957510581538951, -2.116249999999859632, 0.7266254446581354998 ) ) ;
#1927=VERTEX_POINT ( 'NONE', #4988 ) ;
#1935=CARTESIAN_POINT ( 'NONE',  ( 2.975116562878357129, -6.092963562372954556, -1.986801736614415947 ) ) ;
#1936=CARTESIAN_POINT ( 'NONE',  ( 2.195116763761142398, -0.4287499999998638511, 3.287093781494352385 ) ) ;
#1940=CARTESIAN_POINT ( 'NONE',  ( -1.898222722261231343, -2.671874999999975131, 3.554431989243950873 ) ) ;
#1944=DIRECTION ( 'NONE',  ( -1.000000000000000000, -7.475397945009582610E-16, 0.000000000000000000 ) ) ;
#1953=ORIENTED_EDGE ( 'NONE', *, *, #53, .T. ) ;
#1962=CYLINDRICAL_SURFACE ( 'NONE', #9589, 0.8000000000000113687 ) ;
#1967=CARTESIAN_POINT ( 'NONE',  ( 2.925834059445412638, -5.103531737064111340, -2.249496179459815615 ) ) ;
#1972=CARTESIAN_POINT ( 'NONE',  ( -1.183270876295518859, -2.296088562372991859, -3.904436448084174227 ) ) ;
#1975=APPLICATION_CONTEXT ( 'automotive_design' ) ;
#1984=CARTESIAN_POINT ( 'NONE',  ( 3.721607743032638638, -5.000000000000047073, 0.0009661164014421728431 ) ) ;
#1988=CARTESIAN_POINT ( 'NONE',  ( 1.403561989263863629E-14, -5.500000000000003553, 0.000000000000000000 ) ) ;
#1992=EDGE_CURVE ( 'NONE', #7901, #1380, #5221, .T. ) ;
#2003=CARTESIAN_POINT ( 'NONE',  ( -2.306523490862328885, -5.639838562372902153, 2.812621923907788091 ) ) ;
#2004=CARTESIAN_POINT ( 'NONE',  ( 0.7459506331255062461, -1.366249999999944897, 3.755271276440939054 ) ) ;
#2007=CARTESIAN_POINT ( 'NONE',  ( -3.144577161339557669, -2.390624999999865885, -2.578777943664209982 ) ) ;
#2011=CARTESIAN_POINT ( 'NONE',  ( -4.166404709851690313, -1.484374999999892752, -0.4114723880711238513 ) ) ;
#2013=EDGE_CURVE ( 'NONE', #9382, #10851, #1814, .T. ) ;
#2019=B_SPLINE_CURVE_WITH_KNOTS ( 'NONE', 3,
 ( #9090, #7930, #8235, #7162 ),
 .UNSPECIFIED., .F., .F.,
 ( 4, 4 ),
 ( 2.309401076757279912E-07, 0.002598307151460991539 ),
 .UNSPECIFIED. ) ;
#2028=CARTESIAN_POINT ( 'NONE',  ( -1.647113530155736916, -3.913124999999971099, -3.078783428963292490 ) ) ;
#2036=CARTESIAN_POINT ( 'NONE',  ( -2.773099908550811676, -0.4995676945082661580, 3.130259945877469363 ) ) ;
#2039=EDGE_CURVE ( 'NONE', #7102, #3975, #9641, .T. ) ;
#2048=B_SPLINE_CURVE_WITH_KNOTS ( 'NONE', 3,
 ( #11751, #3374, #2439, #7258, #6947, #4698, #8180, #10416, #14147, #9260, #14224, #13998 ),
 .UNSPECIFIED., .F., .F.,
 ( 4, 2, 2, 2, 2, 4 ),
 ( 2.544323688695603672E-07, 0.001342108318545691186, 0.002013035261634101361, 0.002683962204722511753, 0.004025816090899332102, 0.005367669977076152885 ),
 .UNSPECIFIED. ) ;
#2051=CARTESIAN_POINT ( 'NONE',  ( 2.831777009049577298, -2.874213562372941677, 2.829717318554673788 ) ) ;
#2056=ADVANCED_FACE ( 'NONE', ( #7638 ), #11181, .T. ) ;
#2064=CARTESIAN_POINT ( 'NONE',  ( 3.756292859848885168, -0.6318749999998841682, -1.140955529460069950 ) ) ;
#2066=CARTESIAN_POINT ( 'NONE',  ( -1.090659875871078599, -1.881874999999897824, -3.598793876473114661 ) ) ;
#2070=CARTESIAN_POINT ( 'NONE',  ( 3.953167801354152022, -0.4995676945082486720, 0.3853396878248828150 ) ) ;
#2077=ORIENTED_EDGE ( 'NONE', *, *, #13386, .F. ) ;
#2079=CARTESIAN_POINT ( 'NONE',  ( -3.406603204915187533, -4.053749999999936016, -0.6763000812039869913 ) ) ;
#2083=CARTESIAN_POINT ( 'NONE',  ( -3.385045168076599165, -5.436713562373150843, -1.403157895329555593 ) ) ;
#2084=CARTESIAN_POINT ( 'NONE',  ( -2.814361612698371928, -0.2100000000001143730, 2.816411668391514578 ) ) ;
#2085=CARTESIAN_POINT ( 'NONE',  ( 1.161840668242749786, -5.408364452671047928, 3.095256225502303948 ) ) ;
#2086=CARTESIAN_POINT ( 'NONE',  ( 1.163914675889782702, -2.796875000000069722, 3.840555497293599352 ) ) ;
#2105=CARTESIAN_POINT ( 'NONE',  ( -2.874539946219666575, -4.178749999999989306, 1.919644203647528302 ) ) ;
#2106=FACE_OUTER_BOUND ( 'NONE', #919, .T. ) ;
#2122=CARTESIAN_POINT ( 'NONE',  ( -2.641694630006354405, -1.640624999999979572, 3.221290409975102520 ) ) ;
#2124=COLOUR_RGB ( '', 0.08235294, 0.09019608, 0.10196078) ;
#2126=CARTESIAN_POINT ( 'NONE',  ( -0.7860821048245157927, -2.717963562373058473, 3.946463394123028490 ) ) ;
#2128=CONICAL_SURFACE ( 'NONE', #6616, 3.173335668876520632, 0.9162978572970248425 ) ;
#2141=CARTESIAN_POINT ( 'NONE',  ( -3.640012805681923869, -5.484374212848019958, -0.3571734599629662332 ) ) ;
#2145=CARTESIAN_POINT ( 'NONE',  ( -3.581969766213484174, -3.100624999999847198, 0.3518610084922548231 ) ) ;
#2154=DIRECTION ( 'NONE',  ( 0.9848077530122082424, 0.1736481776669299149, 0.000000000000000000 ) ) ;
#2161=CARTESIAN_POINT ( 'NONE',  ( 2.762998497935824194, -6.108588562373387987, -2.269244778944577323 ) ) ;
#2162=CARTESIAN_POINT ( 'NONE',  ( -2.135074830120813782, -1.241249999999904707, 3.197897516496418291 ) ) ;
#2163=CARTESIAN_POINT ( 'NONE',  ( 3.325473450044490242, -2.906249999999835243, 2.220260485081660740 ) ) ;
#2165=FACE_OUTER_BOUND ( 'NONE', #2197, .T. ) ;
#2170=CARTESIAN_POINT ( 'NONE',  ( -9.797174393178965434E-17, 9.500000000000000000, 0.000000000000000000 ) ) ;
#2174=ORIENTED_EDGE ( 'NONE', *, *, #3354, .T. ) ;
#2181=CARTESIAN_POINT ( 'NONE',  ( -1.318845896519720284, -4.272500000000155396, 3.181678407182404023 ) ) ;
#2191=ORIENTED_EDGE ( 'NONE', *, *, #5274, .T. ) ;
#2192=LINE ( 'NONE', #9473, #3647 ) ;
#2197=EDGE_LOOP ( 'NONE', ( #4531, #2968, #2811, #2542, #7497, #9058, #12496 ) ) ;
#2199=CARTESIAN_POINT ( 'NONE',  ( -4.100362740845592491, -1.531249999999860556, 0.8144810970459482879 ) ) ;
#2201=CARTESIAN_POINT ( 'NONE',  ( 3.622844214532213503, -2.077338562372990527, -1.938139479208375038 ) ) ;
#2213=CARTESIAN_POINT ( 'NONE',  ( 3.931950937192210116, -0.5849999999998678479, -0.001434051515494263150 ) ) ;
#2215=CARTESIAN_POINT ( 'NONE',  ( -3.093239089446854884, -2.178749999999916476, 2.068481483294962953 ) ) ;
#2216=CARTESIAN_POINT ( 'NONE',  ( -1.006616814747114486E-29, -2.568816543514388222E-44, -4.500000000000000888 ) ) ;
#2220=DIRECTION ( 'NONE',  ( 1.000000000000000000, 0.000000000000000000, 1.224646799147353454E-16 ) ) ;
#2230=CARTESIAN_POINT ( 'NONE',  ( -2.669536895096369378, -4.194375000000057696, 2.192493760422842719 ) ) ;
#2234=CARTESIAN_POINT ( 'NONE',  ( 3.646332799887131770, -5.030463562373060249, -0.7266944397774037778 ) ) ;
#2236=DIRECTION ( 'NONE',  ( 0.4999999999999999445, 0.000000000000000000, -0.8660254037844387076 ) ) ;
#2244=CARTESIAN_POINT ( 'NONE',  ( -3.322613055092911161, -5.069375000000116316, -0.3280989749989032256 ) ) ;
#2253=CARTESIAN_POINT ( 'NONE',  ( -1.914696782014857490, -4.241249999999832987, 2.867854448260447775 ) ) ;
#2258=AXIS2_PLACEMENT_3D ( 'NONE', #11439, #804, #9105 ) ;
#2263=CONICAL_SURFACE ( 'NONE', #13917, 4.500000000000000888, 1.396263401595466691 ) ;
#2271=CARTESIAN_POINT ( 'NONE',  ( 1.991706217211437036, -1.171874999999983347, -3.729459312589495923 ) ) ;
#2273=CARTESIAN_POINT ( 'NONE',  ( -3.884733793026120541, -2.452338562373202802, -1.176880867913740358 ) ) ;
#2282=CARTESIAN_POINT ( 'NONE',  ( 2.937061643673781752, -5.103115294876279684, -2.234448363260541193 ) ) ;
#2288=CARTESIAN_POINT ( 'NONE',  ( 2.769370807496426945, -0.7100000000000333822, -2.767918543042355850 ) ) ;
#2290=CARTESIAN_POINT ( 'NONE',  ( 1.096135970525389913, -1.788124999999989750, -3.610092524386871560 ) ) ;
#2296=AXIS2_PLACEMENT_3D ( 'NONE', #9454, #3721, #1314 ) ;
#2300=AXIS2_PLACEMENT_3D ( 'NONE', #4167, #1908, #10191 ) ;
#2304=EDGE_CURVE ( 'NONE', #14968, #1927, #3801, .T. ) ;
#2305=ORIENTED_EDGE ( 'NONE', *, *, #3996, .T. ) ;
#2306=CARTESIAN_POINT ( 'NONE',  ( 0.001278483876778065912, -4.335000000000164277, 3.435880605283331946 ) ) ;
#2312=CARTESIAN_POINT ( 'NONE',  ( 2.080555833684100797, -4.842963562373058473, 3.111297368939876407 ) ) ;
#2315=CIRCLE ( 'NONE', #574, 0.8000000000000176970 ) ;
#2316=CARTESIAN_POINT ( 'NONE',  ( -2.598076211353319120, 1.678847577293364424, 4.500000000000000888 ) ) ;
#2325=CARTESIAN_POINT ( 'NONE',  ( -3.196762997434627440, -4.147500000000007958, 1.325534829466321840 ) ) ;
#2335=CARTESIAN_POINT ( 'NONE',  ( 2.024885806073651651, -2.741249999999974207, -3.032875982375832891 ) ) ;
#2339=CARTESIAN_POINT ( 'NONE',  ( 2.372013019084901586, -4.859374999999952927, 2.891838320553053343 ) ) ;
#2353=CARTESIAN_POINT ( 'NONE',  ( 3.641294513787672660, -1.921088562373076236, 1.947552941946255389 ) ) ;
#2367=CARTESIAN_POINT ( 'NONE',  ( -3.745604523531179897, -3.546874999999923173, 1.135144126415479793 ) ) ;
#2370=ADVANCED_FACE ( 'NONE', ( #9532 ), #3654, .T. ) ;
#2371=CARTESIAN_POINT ( 'NONE',  ( -2.463482987169076210, -0.9443750000000532552, -3.003366100166337649 ) ) ;
#2372=CARTESIAN_POINT ( 'NONE',  ( -0.5946215730125156140, -5.371277108568085268, 3.300960504506171400 ) ) ;
#2378=CIRCLE ( 'NONE', #12053, 2.514916625122320948 ) ;
#2382=DIRECTION ( 'NONE',  ( -1.000000000000000000, -9.422394424380278809E-16, 0.000000000000000000 ) ) ;
#2387=CARTESIAN_POINT ( 'NONE',  ( -2.013335231365205313, -2.928749999999985310, -3.010762893885848168 ) ) ;
#2393=AXIS2_PLACEMENT_3D ( 'NONE', #14035, #4728, #2236 ) ;
#2394=CARTESIAN_POINT ( 'NONE',  ( -3.140138096963257297, -4.592963562373083342, 2.096990760703472567 ) ) ;
#2402=CARTESIAN_POINT ( 'NONE',  ( -2.874539946219666575, -4.178749999999989306, 1.919644203647528302 ) ) ;
#2409=VERTEX_POINT ( 'NONE', #4970 ) ;
#2413=CARTESIAN_POINT ( 'NONE',  ( -3.586083906644841779, -3.069375000000151399, -0.3518610084925551384 ) ) ;
#2417=CARTESIAN_POINT ( 'NONE',  ( -1.770063184912698206, 2.057215485424382262, -4.499999999999998224 ) ) ;
#2423=FACE_OUTER_BOUND ( 'NONE', #7051, .T. ) ;
#2433=CARTESIAN_POINT ( 'NONE',  ( 2.767528002676985288, -0.1406250000000294209, -3.374716907253854092 ) ) ;
#2436=CARTESIAN_POINT ( 'NONE',  ( -3.223041131337215592, -1.608588562373021835, 2.647033509805598150 ) ) ;
#2439=CARTESIAN_POINT ( 'NONE',  ( 4.785585838562195882, 2.054436331234747115, -0.7111221836281572672 ) ) ;
#2441=EDGE_LOOP ( 'NONE', ( #13075, #1953, #7685 ) ) ;
#2442=CARTESIAN_POINT ( 'NONE',  ( -3.637955631634631981, -5.500000000000017764, 0.000000000000000000 ) ) ;
#2446=CARTESIAN_POINT ( 'NONE',  ( 2.736090332400194836, -3.875000000000003553, 2.737522629006357455 ) ) ;
#2447=ORIENTED_EDGE ( 'NONE', *, *, #13031, .F. ) ;
#2448=CARTESIAN_POINT ( 'NONE',  ( 2.481497852716095132, -0.7256250000000298295, -3.025965195089417747 ) ) ;
#2449=CARTESIAN_POINT ( 'NONE',  ( 1.430388965971081561, -5.414568188701776030, 2.971966112566031715 ) ) ;
#2460=CARTESIAN_POINT ( 'NONE',  ( -2.533829858540610047, -3.209999999999945786, 2.535703909530143463 ) ) ;
#2462=ORIENTED_EDGE ( 'NONE', *, *, #1726, .T. ) ;
#2473=CARTESIAN_POINT ( 'NONE',  ( -1.318845896519720284, -4.272500000000155396, 3.181678407182404023 ) ) ;
#2479=ORIENTED_EDGE ( 'NONE', *, *, #2304, .T. ) ;
#2500=CARTESIAN_POINT ( 'NONE',  ( 0.4250114624652890916, -0.2343749999999928668, -4.331188314191872557 ) ) ;
#2502=CARTESIAN_POINT ( 'NONE',  ( -2.312421387223750902, -1.655463562372999187, 3.463495667214802953 ) ) ;
#2520=CARTESIAN_POINT ( 'NONE',  ( 0.7330380326264336333, -4.781250000000259348, 3.678172007241774732 ) ) ;
#2523=CARTESIAN_POINT ( 'NONE',  ( 3.756292859848789689, -0.6318749999998841682, -1.140955529460117690 ) ) ;
#2526=CIRCLE ( 'NONE', #2773, 2.320576762250993852 ) ;
#2529=CARTESIAN_POINT ( 'NONE',  ( 5.196152422706631135, 0.1227504548087541975, -1.122964458370237425E-15 ) ) ;
#2530=CARTESIAN_POINT ( 'NONE',  ( 2.188996733326721955, -5.387487143035719406, 2.513283957937794355 ) ) ;
#2540=CARTESIAN_POINT ( 'NONE',  ( 0.3508518002069098141, -3.350624999999907150, 3.548798009676431331 ) ) ;
#2542=ORIENTED_EDGE ( 'NONE', *, *, #8874, .F. ) ;
#2549=LINE ( 'NONE', #7298, #13097 ) ;
#2552=CARTESIAN_POINT ( 'NONE',  ( -1.914696782014857490, -4.241249999999832987, 2.867854448260447775 ) ) ;
#2563=DIRECTION ( 'NONE',  ( 2.551930889570660354E-15, -1.000000000000000000, 0.000000000000000000 ) ) ;
#2564=CARTESIAN_POINT ( 'NONE',  ( -0.7342670381812395064, -4.718750000000252243, 3.686397723581088304 ) ) ;
#2576=EDGE_LOOP ( 'NONE', ( #2479, #7271 ) ) ;
#2582=CARTESIAN_POINT ( 'NONE',  ( -2.047045606697944109, -0.3281249999999383271, -3.826439644639493487 ) ) ;
#2583=CARTESIAN_POINT ( 'NONE',  ( -3.327015569456945876, -0.6085885623731795979, 2.728925429665365776 ) ) ;
#2588=DIRECTION ( 'NONE',  ( 9.422394424380278809E-16, -1.000000000000000000, 0.000000000000000000 ) ) ;
#2597=CARTESIAN_POINT ( 'NONE',  ( -1.460276376564476175, -4.312500000000168754, -3.521769549316223102 ) ) ;
#2604=CARTESIAN_POINT ( 'NONE',  ( -3.844997831300932756, -1.100624999999974429, 0.3801187285354425405 ) ) ;
#2605=CARTESIAN_POINT ( 'NONE',  ( -1.165664718218115015, -5.359101102505690051, 3.151588464108890264 ) ) ;
#2607=EDGE_CURVE ( 'NONE', #9386, #8682, #10293, .T. ) ;
#2613=CLOSED_SHELL ( 'NONE', ( #12366, #7367, #2056, #6299, #7918, #10068, #2915, #8105, #5476, #8957, #8780, #4692, #12623, #7735, #12757, #6698, #1675, #5462, #7135, #10168, #532, #12253, #899, #10008, #6937, #14155, #14929, #3162, #4325, #1381, #5487, #14829, #14357, #8586, #1446, #8672, #12538, #13439, #10430, #3236, #5236, #2370, #456 ) ) ;
#2615=CONICAL_SURFACE ( 'NONE', #376, 4.500000000000000888, 0.7853981633974500554 ) ;
#2622=CARTESIAN_POINT ( 'NONE',  ( -1.685726645313963656, -3.256874999999974651, 3.156579729352138930 ) ) ;
#2632=CARTESIAN_POINT ( 'NONE',  ( -1.266185496994490789, -5.191497722025411932, -3.348809276478283081 ) ) ;
#2642=ORIENTED_EDGE ( 'NONE', *, *, #13031, .T. ) ;
#2643=VERTEX_POINT ( 'NONE', #13868 ) ;
#2647=CARTESIAN_POINT ( 'NONE',  ( 1.363531154075378282, -3.397500000000037712, 3.288412936073061399 ) ) ;
#2649=CARTESIAN_POINT ( 'NONE',  ( 0.7448305450414310913, -4.218749999999887201, -3.751694669322447329 ) ) ;
#2659=DIRECTION ( 'NONE',  ( -2.551930889570659960E-15, 1.000000000000000000, 0.000000000000000000 ) ) ;
#2661=B_SPLINE_CURVE_WITH_KNOTS ( 'NONE', 3,
 ( #12820, #10397, #6929, #13900, #12979, #13065, #6857, #11647, #4518, #11881, #5771, #2417, #9392, #9464 ),
 .UNSPECIFIED., .F., .F.,
 ( 4, 2, 2, 2, 2, 2, 4 ),
 ( 0.002714574482386751184, 0.003387943617500365975, 0.004061312752613980767, 0.005408051022841208616, 0.006081420157954823408, 0.006754789293068438200, 0.008101527563295666048 ),
 .UNSPECIFIED. ) ;
#2663=CARTESIAN_POINT ( 'NONE',  ( -3.336666538900097123, -5.084999999999988418, 0.001247370357356067296 ) ) ;
#2667=CARTESIAN_POINT ( 'NONE',  ( 0.001503091390574608048, -1.749213562373128195, 4.152102130272123937 ) ) ;
#2680=CARTESIAN_POINT ( 'NONE',  ( 1.766265845880009788, -4.828125000000014211, 3.301533676270316686 ) ) ;
#2682=CARTESIAN_POINT ( 'NONE',  ( -3.719851489431995173, -4.467963562373030051, -0.7385069234750470946 ) ) ;
#2684=CARTESIAN_POINT ( 'NONE',  ( -2.976231983981160845, -1.194374999999927578, 2.444352914378567387 ) ) ;
#2699=CARTESIAN_POINT ( 'NONE',  ( 3.059130242547762002, -2.491250000000117204, 2.045191655759115434 ) ) ;
#2705=CARTESIAN_POINT ( 'NONE',  ( 2.400236239102856661, -5.117328313055176103, -2.785141875113248844 ) ) ;
#2708=CARTESIAN_POINT ( 'NONE',  ( 3.039268535905459423, -0.4995676945082513920, -2.698502599271650038 ) ) ;
#2719=CARTESIAN_POINT ( 'NONE',  ( 3.503842902704710216, -2.631874999999911147, -1.061889326425361268 ) ) ;
#2721=CARTESIAN_POINT ( 'NONE',  ( -3.787710864223658991, -4.499999999999990230, 0.001388818612877307929 ) ) ;
#2734=CARTESIAN_POINT ( 'NONE',  ( -3.199287326323787539, -5.038124999999881837, -0.9691876696830880045 ) ) ;
#2736=CARTESIAN_POINT ( 'NONE',  ( -2.785343681203863664, -4.991249999999938680, -1.859602269982785883 ) ) ;
#2739=CARTESIAN_POINT ( 'NONE',  ( -1.629699455448989389E-14, 8.699999999999999289, 5.655858585055787181E-29 ) ) ;
#2747=CARTESIAN_POINT ( 'NONE',  ( 2.225207906715364281, -2.843749999999932943, 3.332158947996217702 ) ) ;
#2749=CARTESIAN_POINT ( 'NONE',  ( -2.691423129642354084, -4.374213562373147290, -2.689451441446156554 ) ) ;
#2770=CARTESIAN_POINT ( 'NONE',  ( -1.439523803302256599, -1.897500000000171383, -3.471712813344601578 ) ) ;
#2773=AXIS2_PLACEMENT_3D ( 'NONE', #12585, #12353, #1944 ) ;
#2775=CARTESIAN_POINT ( 'NONE',  ( -3.036530611102517874, -5.238391572205651769, -1.778739313110275999 ) ) ;
#2794=CARTESIAN_POINT ( 'NONE',  ( 1.096135970525389913, -1.788124999999989750, -3.610092524386871560 ) ) ;
#2798=CARTESIAN_POINT ( 'NONE',  ( 3.833377307806092649, -4.015625000000129674, -0.3765428855675501119 ) ) ;
#2811=ORIENTED_EDGE ( 'NONE', *, *, #11069, .F. ) ;
#2816=CARTESIAN_POINT ( 'NONE',  ( 3.135427973343691832, -5.538124999999991971, 0.9519854854112211884 ) ) ;
#2819=CARTESIAN_POINT ( 'NONE',  ( -2.488972454571050985, -5.975625000000068354, -2.041081048424583155 ) ) ;
#2832=( NAMED_UNIT ( * ) SI_UNIT ( $, .STERADIAN. ) SOLID_ANGLE_UNIT ( ) );
#2833=CARTESIAN_POINT ( 'NONE',  ( -2.264039642164870969, -2.343749999999985789, -3.385713959793517080 ) ) ;
#2839=DIRECTION ( 'NONE',  ( -1.000000000000000000, 0.000000000000000000, 0.000000000000000000 ) ) ;
#2843=CARTESIAN_POINT ( 'NONE',  ( -0.2250800284370903792, 2.375126721000841101, 4.500000000000000888 ) ) ;
#2850=EDGE_LOOP ( 'NONE', ( #1376, #839, #3022, #1061 ) ) ;
#2852=CARTESIAN_POINT ( 'NONE',  ( 3.783562653031028677, -1.569374999999871845, 0.3712484392075320883 ) ) ;
#2861=CARTESIAN_POINT ( 'NONE',  ( -3.121185083186896581, -0.4995676945082675457, -2.860075285120150301 ) ) ;
#2878=CARTESIAN_POINT ( 'NONE',  ( -3.579091221414520518, -2.038125000000108322, -1.084269867492441586 ) ) ;
#2880=CARTESIAN_POINT ( 'NONE',  ( 2.968551569176787197, -4.109374999999867661, -2.434929705433495073 ) ) ;
#2884=CARTESIAN_POINT ( 'NONE',  ( -0.4212280308283230523, -0.7343750000000048850, 4.265137983724988757 ) ) ;
#2892=CARTESIAN_POINT ( 'NONE',  ( 3.250000000000017764, 7.362500000000000711, 0.000000000000000000 ) ) ;
#2897=CARTESIAN_POINT ( 'NONE',  ( 2.729225460314726348, -5.491250000000120757, 1.824606648063346048 ) ) ;
#2900=CARTESIAN_POINT ( 'NONE',  ( 0.6449049195797605938, -5.366250000000259313, 3.235821967343390337 ) ) ;
#2904=DIRECTION ( 'NONE',  ( -0.4999999999999997780, 0.000000000000000000, -0.8660254037844387076 ) ) ;
#2907=CARTESIAN_POINT ( 'NONE',  ( -0.8000000000000114797, 9.500000000000000000, 0.000000000000000000 ) ) ;
#2910=EDGE_LOOP ( 'NONE', ( #10609, #3507, #13262, #13277, #12712, #13912 ) ) ;
#2915=ADVANCED_FACE ( 'NONE', ( #14170 ), #9501, .T. ) ;
#2918=CARTESIAN_POINT ( 'NONE',  ( 2.601763032574845536, -2.140624999999891198, -3.168547547573197232 ) ) ;
#2933=AXIS2_PLACEMENT_3D ( 'NONE', #11028, #400, #8694 ) ;
#2935=CARTESIAN_POINT ( 'NONE',  ( -3.844997831300933200, -1.100624999999974429, 0.3801187285354191148 ) ) ;
#2936=EDGE_LOOP ( 'NONE', ( #10936, #7404, #8287, #10034 ) ) ;
#2937=DIRECTION ( 'NONE',  ( 1.000000000000000000, 2.551930889570660354E-15, 0.000000000000000000 ) ) ;
#2953=EDGE_CURVE ( 'NONE', #3303, #9068, #10755, .T. ) ;
#2954=CARTESIAN_POINT ( 'NONE',  ( 3.380062874710183074, -2.647499999999996856, -1.401527478686670491 ) ) ;
#2955=CARTESIAN_POINT ( 'NONE',  ( -2.431404194366994176, 4.650702586819541295, 0.000000000000000000 ) ) ;
#2956=CARTESIAN_POINT ( 'NONE',  ( 1.111882196364886832, -4.203124999999903189, -3.661942331401731199 ) ) ;
#2961=CARTESIAN_POINT ( 'NONE',  ( -0.4147139277428218418, -1.265625000000086819, -4.195123116704944088 ) ) ;
#2968=ORIENTED_EDGE ( 'NONE', *, *, #10785, .F. ) ;
#2969=ORIENTED_EDGE ( 'NONE', *, *, #4892, .T. ) ;
#2974=CARTESIAN_POINT ( 'NONE',  ( 3.211975673186791447, -5.553749999999917364, 0.6376497042497289991 ) ) ;
#2981=CARTESIAN_POINT ( 'NONE',  ( -0.3313405146688110925, -4.850625000000119869, -3.351331461923120703 ) ) ;
#2987=CARTESIAN_POINT ( 'NONE',  ( 2.807699568699258297, -3.124999999999853895, -2.806223270957961091 ) ) ;
#2990=CARTESIAN_POINT ( 'NONE',  ( -1.131278458607941850, -3.702338562373107322, 3.725811129568937563 ) ) ;
#3006=CARTESIAN_POINT ( 'NONE',  ( 2.577850803773711785, 4.297149196226276224, -4.769823568025666751E-16 ) ) ;
#3007=CARTESIAN_POINT ( 'NONE',  ( 3.730555813499152329, -1.553749999999926246, 0.7430650243616526707 ) ) ;
#3021=ORIENTED_EDGE ( 'NONE', *, *, #10959, .F. ) ;
#3022=ORIENTED_EDGE ( 'NONE', *, *, #10869, .F. ) ;
#3024=CARTESIAN_POINT ( 'NONE',  ( 0.7073082199525939640, -5.780463562373353348, 3.549031173911244341 ) ) ;
#3026=CARTESIAN_POINT ( 'NONE',  ( -3.456628223078394679, -2.022499999999918252, -1.432834870345867984 ) ) ;
#3028=CARTESIAN_POINT ( 'NONE',  ( -4.034970194612536254, -2.484375000000152767, -0.3959303163385184399 ) ) ;
#3032=CARTESIAN_POINT ( 'NONE',  ( -3.331139167509281851, 2.239389106484336978, -3.230297714791236174 ) ) ;
#3033=CARTESIAN_POINT ( 'NONE',  ( 2.992932217727461097, -1.124999999999971800, -2.995094308971279151 ) ) ;
#3039=TOROIDAL_SURFACE ( 'NONE', #791, 2.931404194366992400, 0.5000000000000000000 ) ;
#3046=CARTESIAN_POINT ( 'NONE',  ( 2.709518412118975039, -5.678749999999861409, -1.809455179588198792 ) ) ;
#3047=DIRECTION ( 'NONE',  ( 9.422394424380278809E-16, -1.000000000000000000, 0.000000000000000000 ) ) ;
#3048=DIRECTION ( 'NONE',  ( 0.8660254037844388186, 2.210036979070413080E-15, -0.4999999999999998335 ) ) ;
#3052=CARTESIAN_POINT ( 'NONE',  ( -0.09826241581420043503, -0.4995676945082593856, 4.080646605992279241 ) ) ;
#3054=CARTESIAN_POINT ( 'NONE',  ( -2.785343681203863664, -4.991249999999938680, -1.859602269982785883 ) ) ;
#3064=CARTESIAN_POINT ( 'NONE',  ( -3.736626632189893105, -2.562500000000080824, 1.546606261444747554 ) ) ;
#3081=EDGE_CURVE ( 'NONE', #3975, #8406, #7411, .T. ) ;
#3082=CARTESIAN_POINT ( 'NONE',  ( -3.115386749435267610, -1.991250000000079678, -2.079980318098562542 ) ) ;
#3087=CARTESIAN_POINT ( 'NONE',  ( 2.598076211353311127, 1.678847577293378190, 4.500000000000000000 ) ) ;
#3102=CARTESIAN_POINT ( 'NONE',  ( -0.3539834606290251928, -5.733588562373254760, 3.607703032259661935 ) ) ;
#3104=CARTESIAN_POINT ( 'NONE',  ( 1.843713500184339216, -0.7568749999999383471, -3.447171040406491027 ) ) ;
#3108=CARTESIAN_POINT ( 'NONE',  ( 2.225207906715364281, -2.843749999999932943, 3.332158947996217702 ) ) ;
#3111=CARTESIAN_POINT ( 'NONE',  ( 2.801070059014833191, 1.881841424954898923, 4.148404342226347907 ) ) ;
#3112=CARTESIAN_POINT ( 'NONE',  ( 4.232448940998905229, -0.9843749999998714362, 0.4153177470904050317 ) ) ;
#3124=CARTESIAN_POINT ( 'NONE',  ( -3.196762997434627440, -4.147500000000007958, 1.325534829466321840 ) ) ;
#3127=CARTESIAN_POINT ( 'NONE',  ( 2.093999815491831562, 9.250000000000001776, 0.000000000000000000 ) ) ;
#3131=CARTESIAN_POINT ( 'NONE',  ( -0.3199098613971397276, -0.4995676945082599407, 4.077077341688482015 ) ) ;
#3134=CARTESIAN_POINT ( 'NONE',  ( -1.562933739280453205, -5.256875000000181153, 2.922265072135110220 ) ) ;
#3142=CARTESIAN_POINT ( 'NONE',  ( -0.4147139277428218418, -1.265625000000086819, -4.195123116704944088 ) ) ;
#3144=CARTESIAN_POINT ( 'NONE',  ( 3.305159631054613634, -3.092963562373059805, -2.207179784781822196 ) ) ;
#3153=DIRECTION ( 'NONE',  ( -9.422394424380278809E-16, 1.000000000000000000, -0.000000000000000000 ) ) ;
#3158=CARTESIAN_POINT ( 'NONE',  ( -3.516205069202407163, -0.1631249999999115075, 1.881096664271727059 ) ) ;
#3162=ADVANCED_FACE ( 'NONE', ( #14859 ), #13971, .T. ) ;
#3172=CARTESIAN_POINT ( 'NONE',  ( 0.6449049195797814660, -5.366250000000259313, 3.235821967343390781 ) ) ;
#3175=VERTEX_POINT ( 'NONE', #7753 ) ;
#3178=CARTESIAN_POINT ( 'NONE',  ( -1.487946254897619447, -0.8975000000000187272, -3.594883137563858355 ) ) ;
#3182=CARTESIAN_POINT ( 'NONE',  ( 3.986138996993924266, -2.999999999999990674, -0.001451045610905104914 ) ) ;
#3195=EDGE_CURVE ( 'NONE', #12756, #7247, #11649, .T. ) ;
#3199=CARTESIAN_POINT ( 'NONE',  ( 3.151910583997929116, -4.522499999999531894, 1.304188709559700232 ) ) ;
#3213=CARTESIAN_POINT ( 'NONE',  ( -2.783274248898092385, -3.374213562373101105, -2.784736148173822201 ) ) ;
#3219=DIRECTION ( 'NONE',  ( -1.747085166004344019E-15, 1.000000000000000000, -0.000000000000000000 ) ) ;
#3221=EDGE_LOOP ( 'NONE', ( #8785, #58, #4258 ) ) ;
#3223=CARTESIAN_POINT ( 'NONE',  ( -1.070211464245647282, -5.296874999999768185, -3.523343936188056968 ) ) ;
#3226=CARTESIAN_POINT ( 'NONE',  ( -0.7073002561900942897, -2.866249999999988418, -3.560643744722076232 ) ) ;
#3227=CARTESIAN_POINT ( 'NONE',  ( -1.733190484027920863, 0.04649911033017210121, -4.499999999999999112 ) ) ;
#3235=PRODUCT_DEFINITION ( 'UNKNOWN', '', #4274, #778 ) ;
#3236=ADVANCED_FACE ( 'NONE', ( #14015 ), #7301, .F. ) ;
#3238=ORIENTED_EDGE ( 'NONE', *, *, #125, .T. ) ;
#3239=CARTESIAN_POINT ( 'NONE',  ( 2.393563981450126388, -4.710000000000058584, -2.395350030107681327 ) ) ;
#3244=CARTESIAN_POINT ( 'NONE',  ( 3.441012398922143056, -5.952338562373084230, 1.044788167591881534 ) ) ;
#3245=CARTESIAN_POINT ( 'NONE',  ( 3.852585042300790352, -0.6162500000000914469, -0.7652758215885018256 ) ) ;
#3248=CARTESIAN_POINT ( 'NONE',  ( 3.946741062051739579, -1.953124999999941380, 1.198372487375103157 ) ) ;
#3249=DIRECTION ( 'NONE',  ( 1.000000000000000000, 0.000000000000000000, 0.000000000000000000 ) ) ;
#3253=DIRECTION ( 'NONE',  ( 1.000000000000000000, 8.284258017326334836E-16, 0.000000000000000000 ) ) ;
#3261=CIRCLE ( 'NONE', #543, 3.173335668876520188 ) ;
#3266=CARTESIAN_POINT ( 'NONE',  ( -3.325293793763300698, -4.038125000000090559, -1.009645679448947231 ) ) ;
#3279=CARTESIAN_POINT ( 'NONE',  ( 2.093999815491831562, 9.500000000000001776, 0.000000000000000000 ) ) ;
#3286=CARTESIAN_POINT ( 'NONE',  ( 3.275404563695782034, -1.109375000000065503, -2.686596450795923463 ) ) ;
#3289=CARTESIAN_POINT ( 'NONE',  ( 3.173589072176457027, -2.108588562373159725, -2.603092057013398186 ) ) ;
#3302=CARTESIAN_POINT ( 'NONE',  ( 3.654380903460823671, -4.968749999999916511, 0.7255053565382596492 ) ) ;
#3303=VERTEX_POINT ( 'NONE', #5898 ) ;
#3304=CARTESIAN_POINT ( 'NONE',  ( 2.337649614532405717, -2.444375000000051479, 2.849939602875970035 ) ) ;
#3313=CARTESIAN_POINT ( 'NONE',  ( -3.466497813382189541, -5.275048774667015827, -7.182839392716466875E-16 ) ) ;
#3320=CARTESIAN_POINT ( 'NONE',  ( 2.619799856955865369, -4.694374999999869402, -2.148899555557211904 ) ) ;
#3325=CARTESIAN_POINT ( 'NONE',  ( -2.463482987169076210, -0.9443750000000532552, -3.003366100166337649 ) ) ;
#3327=CARTESIAN_POINT ( 'NONE',  ( 3.808142666863014281, -3.046875000000033751, -1.156701755244785801 ) ) ;
#3331=CARTESIAN_POINT ( 'NONE',  ( -4.993158575045113956, 1.881841424954880937, 0.3515956577736513711 ) ) ;
#3332=CARTESIAN_POINT ( 'NONE',  ( -4.296251640119561621, -0.4995676945082693776, 0.01637110057554332782 ) ) ;
#3345=CARTESIAN_POINT ( 'NONE',  ( 2.393563981450126388, -4.710000000000058584, -2.395350030107596506 ) ) ;
#3347=CARTESIAN_POINT ( 'NONE',  ( 3.897114317029974462, 9.945166405816860437E-15, 2.249999999999999556 ) ) ;
#3354=EDGE_CURVE ( 'NONE', #5205, #4633, #10510, .T. ) ;
#3365=CARTESIAN_POINT ( 'NONE',  ( 3.298003658611986744, -0.8906249999999793499, 2.704611316345772121 ) ) ;
#3367=CIRCLE ( 'NONE', #5873, 4.296275033669348709 ) ;
#3368=CARTESIAN_POINT ( 'NONE',  ( -2.190848337519055278, -3.342963562373078457, -3.276249760082800222 ) ) ;
#3374=CARTESIAN_POINT ( 'NONE',  ( 4.993158575045104186, 1.881841424954905362, -0.3515956577736533140 ) ) ;
#3379=AXIS2_PLACEMENT_3D ( 'NONE', #14621, #9656, #8221 ) ;
#3385=CARTESIAN_POINT ( 'NONE',  ( 0.7624512442115695121, -0.8037500000000172840, -3.827857439461599398 ) ) ;
#3388=CARTESIAN_POINT ( 'NONE',  ( -1.707523105661799434, -2.913124999999936904, -3.196535590052164810 ) ) ;
#3391=CARTESIAN_POINT ( 'NONE',  ( 2.931404194366990623, 4.650702586819546624, 3.589934763638662607E-16 ) ) ;
#3400=CARTESIAN_POINT ( 'NONE',  ( -0.9979582191392041279, -4.288125000000008846, 3.294238300096191896 ) ) ;
#3402=ORIENTED_EDGE ( 'NONE', *, *, #230, .F. ) ;
#3404=CARTESIAN_POINT ( 'NONE',  ( -0.7460806596055710171, -4.280463562373175712, -3.743634425862352177 ) ) ;
#3409=CARTESIAN_POINT ( 'NONE',  ( -4.296227084909979510, -0.4995677573761841406, -0.01166785054812304046 ) ) ;
#3413=CARTESIAN_POINT ( 'NONE',  ( -2.348309169242665639, -5.210000000000155396, 2.347120911809276400 ) ) ;
#3423=CARTESIAN_POINT ( 'NONE',  ( 0.000000000000000000, 0.000000000000000000, 0.000000000000000000 ) ) ;
#3424=CARTESIAN_POINT ( 'NONE',  ( 3.388605160257775140, -4.569374999999831211, 0.3324735777646720680 ) ) ;
#3427=FACE_OUTER_BOUND ( 'NONE', #8897, .T. ) ;
#3434=ORIENTED_EDGE ( 'NONE', *, *, #4000, .T. ) ;
#3442=CARTESIAN_POINT ( 'NONE',  ( 1.243192046278082774, -0.7968750000001610934, 4.092941397521737912 ) ) ;
#3444=CARTESIAN_POINT ( 'NONE',  ( 4.101399898226999241, -1.983588562372964770, 0.4024520375143380568 ) ) ;
#3456=CARTESIAN_POINT ( 'NONE',  ( -0.001357705120208648440, -5.249999999999984013, -3.688496797837457652 ) ) ;
#3460=CARTESIAN_POINT ( 'NONE',  ( -2.795825449145424191, -2.975624999999864517, -2.292747793747622609 ) ) ;
#3465=DIRECTION ( 'NONE',  ( 1.000000000000000000, 2.551930889570660354E-15, 0.000000000000000000 ) ) ;
#3474=CARTESIAN_POINT ( 'NONE',  ( -3.325293793763386851, -4.038125000000090559, -1.009645679448947453 ) ) ;
#3478=CARTESIAN_POINT ( 'NONE',  ( 2.714559208474450980, -4.124213562372948338, -2.713141310347332968 ) ) ;
#3487=CARTESIAN_POINT ( 'NONE',  ( -2.103997734759339711, -5.225624999999808118, 2.565685703212198021 ) ) ;
#3496=DIRECTION ( 'NONE',  ( 0.000000000000000000, 0.000000000000000000, 1.000000000000000000 ) ) ;
#3497=CARTESIAN_POINT ( 'NONE',  ( -2.557519727433407386, -2.960000000000007958, -2.558839988362045403 ) ) ;
#3507=ORIENTED_EDGE ( 'NONE', *, *, #7893, .T. ) ;
#3515=CARTESIAN_POINT ( 'NONE',  ( 1.688254324138965146, 0.1874999999998931965, 4.071669181187491660 ) ) ;
#3517=CARTESIAN_POINT ( 'NONE',  ( 3.546006434268102137, -0.9054635623730455940, 2.367515899259258649 ) ) ;
#3526=PLANE ( 'NONE',  #11808 ) ;
#3531=ORIENTED_EDGE ( 'NONE', *, *, #518, .F. ) ;
#3533=CARTESIAN_POINT ( 'NONE',  ( -3.249648180954406662, -3.593749999999990230, 2.170113394669044293 ) ) ;
#3536=CARTESIAN_POINT ( 'NONE',  ( 3.667419683216786908, -2.585000000000003517, 0.0009491222189788412963 ) ) ;
#3548=DIRECTION ( 'NONE',  ( -9.422394424380278809E-16, 1.000000000000000000, -0.000000000000000000 ) ) ;
#3551=CARTESIAN_POINT ( 'NONE',  ( -1.336190917661153943, -3.897499999999990195, -3.228188129988408761 ) ) ;
#3553=ORIENTED_EDGE ( 'NONE', *, *, #8440, .F. ) ;
#3556=CARTESIAN_POINT ( 'NONE',  ( 0.3733708913940425034, -4.233588562373078901, -3.805181778647142465 ) ) ;
#3567=AXIS2_PLACEMENT_3D ( 'NONE', #13683, #9017, #13758 ) ;
#3569=CARTESIAN_POINT ( 'NONE',  ( 3.535094671665813593, -3.584999999999991083, -0.001309597400350119394 ) ) ;
#3580=CARTESIAN_POINT ( 'NONE',  ( 3.039561480324906029, -2.678749999999966214, -2.029833227700108544 ) ) ;
#3584=DIRECTION ( 'NONE',  ( 2.551930889570659960E-15, -1.000000000000000000, -0.000000000000000000 ) ) ;
#3591=DIRECTION ( 'NONE',  ( -1.000000000000000000, -2.551930889570659960E-15, 0.000000000000000000 ) ) ;
#3600=CARTESIAN_POINT ( 'NONE',  ( -3.816972974264043028, -0.4218749999999791833, -2.038447964682808422 ) ) ;
#3602=CARTESIAN_POINT ( 'NONE',  ( -2.644124373199357336, -1.639838562373160169, 3.220131994730173197 ) ) ;
#3617=LINE ( 'NONE', #1206, #5348 ) ;
#3618=CARTESIAN_POINT ( 'NONE',  ( -3.787710864223658991, -4.499999999999990230, 0.001388818612877307929 ) ) ;
#3622=CARTESIAN_POINT ( 'NONE',  ( -2.746234728672232173, -0.9599999999999920819, -2.744228674164098436 ) ) ;
#3632=ORIENTED_EDGE ( 'NONE', *, *, #13246, .F. ) ;
#3636=CARTESIAN_POINT ( 'NONE',  ( 1.412068586280953220, -2.397499999999971099, 3.411535633775466980 ) ) ;
#3646=CARTESIAN_POINT ( 'NONE',  ( -4.296274425956841725, -0.5002988223950231017, 0.02453012155904704325 ) ) ;
#3647=VECTOR ( 'NONE', #11584, 1000.000000000000114 ) ;
#3649=CARTESIAN_POINT ( 'NONE',  ( 2.743301530724824744, -3.475625000000028386, 2.252549412313605615 ) ) ;
#3654=SPHERICAL_SURFACE ( 'NONE', #2296, 0.8600000000000014300 ) ;
#3663=LINE ( 'NONE', #4831, #7002 ) ;
#3678=CARTESIAN_POINT ( 'NONE',  ( -2.749513137126650353, -0.3593750000000536238, -3.352117812333079705 ) ) ;
#3680=CARTESIAN_POINT ( 'NONE',  ( -3.489569499876165271, -1.405463562373098663, -2.332997265744571447 ) ) ;
#3693=CARTESIAN_POINT ( 'NONE',  ( -2.115018882620673057, -4.343749999999819700, -3.167137413913937660 ) ) ;
#3695=CARTESIAN_POINT ( 'NONE',  ( -1.113040416940756172, -1.288124999999980425, 3.674042195187707360 ) ) ;
#3707=CARTESIAN_POINT ( 'NONE',  ( 1.656526992905777762, -3.756875000000012399, -3.097233728230821548 ) ) ;
#3718=CARTESIAN_POINT ( 'NONE',  ( -3.406603204915101379, -4.053749999999936016, -0.6763000812039869913 ) ) ;
#3721=DIRECTION ( 'NONE',  ( -6.982962677686266711E-15, -6.579622859988665673E-30, -1.000000000000000000 ) ) ;
#3723=EDGE_LOOP ( 'NONE', ( #13337, #34, #12304 ) ) ;
#3728=CARTESIAN_POINT ( 'NONE',  ( -1.990045403832418236, -3.241250000000046594, 2.976654046991286329 ) ) ;
#3732=CARTESIAN_POINT ( 'NONE',  ( 1.403561989263862998E-14, -5.500000000000001776, 0.000000000000000000 ) ) ;
#3748=CARTESIAN_POINT ( 'NONE',  ( 3.633142546501945791, -0.09374999999992907063, -2.429478397922130384 ) ) ;
#3749=CARTESIAN_POINT ( 'NONE',  ( 4.232830310009522812, -0.9835885623730800109, 0.4180357722217523109 ) ) ;
#3766=CARTESIAN_POINT ( 'NONE',  ( -3.756875241620029282, -3.453125000000005773, -1.140712293363390861 ) ) ;
#3770=CARTESIAN_POINT ( 'NONE',  ( 0.3809421545653356445, -0.8193749999999933031, -3.882302026224086156 ) ) ;
#3782=ORIENTED_EDGE ( 'NONE', *, *, #14908, .T. ) ;
#3783=CARTESIAN_POINT ( 'NONE',  ( 2.598076211353308462, 2.375000000000006661, -4.499999999999999112 ) ) ;
#3784=CARTESIAN_POINT ( 'NONE',  ( -3.184718056276182097, -3.006875000000130083, -1.703323619722392435 ) ) ;
#3790=CARTESIAN_POINT ( 'NONE',  ( -3.471269930600009879, -5.271387000335979955, -0.1844037060100978398 ) ) ;
#3796=CARTESIAN_POINT ( 'NONE',  ( 1.974738715674944078, -3.428749999999933795, 2.957050713271639708 ) ) ;
#3801=CIRCLE ( 'NONE', #6544, 0.8000000000000052625 ) ;
#3809=CARTESIAN_POINT ( 'NONE',  ( -2.013335231365204425, -2.928749999999985310, -3.010762893885847280 ) ) ;
#3811=CARTESIAN_POINT ( 'NONE',  ( 3.056473733825995964, -5.095046775857358767, -2.078780392433921431 ) ) ;
#3816=CARTESIAN_POINT ( 'NONE',  ( 2.598076211353315124, 0.1227504548087477720, 4.500000000000000000 ) ) ;
#3820=CARTESIAN_POINT ( 'NONE',  ( 1.403561989263863629E-14, -5.500000000000003553, 0.000000000000000000 ) ) ;
#3827=CARTESIAN_POINT ( 'NONE',  ( -3.268702447147801227, -5.116250000000009734, 0.6493246907703037474 ) ) ;
#3831=CARTESIAN_POINT ( 'NONE',  ( 4.294990272561590494, -0.03125000000009103135, -0.8531314740103178584 ) ) ;
#3833=CARTESIAN_POINT ( 'NONE',  ( 1.994349568762445069, -1.171088562373031827, -3.728778841834516022 ) ) ;
#3847=CARTESIAN_POINT ( 'NONE',  ( -2.497846391779839248, -3.359374999999932943, -3.045264817802638468 ) ) ;
#3850=CARTESIAN_POINT ( 'NONE',  ( 2.458139144364205109, -3.858588562373032271, 2.993019814648903765 ) ) ;
#3852=CARTESIAN_POINT ( 'NONE',  ( 1.843713500184339216, -0.7568749999999383471, -3.447171040406491027 ) ) ;
#3868=DIRECTION ( 'NONE',  ( -1.000000000000000000, 0.000000000000000000, 6.860497997771530774E-15 ) ) ;
#3869=CARTESIAN_POINT ( 'NONE',  ( 0.3573659033054734091, -2.819374999999921805, -3.618812876704415871 ) ) ;
#3877=CARTESIAN_POINT ( 'NONE',  ( 2.822529449220563258, -0.4995676945082517251, -2.935231339109197091 ) ) ;
#3889=CARTESIAN_POINT ( 'NONE',  ( 2.926652851519762955, -1.694375000000067022, -2.400566300852225776 ) ) ;
#3891=CARTESIAN_POINT ( 'NONE',  ( -3.269128917323805172, -3.406249999999943601, -2.185603562728522853 ) ) ;
#3893=CARTESIAN_POINT ( 'NONE',  ( 7.511572993685698521E-16, 1.916901515185129432E-30, 4.500000000000000888 ) ) ;
#3908=CARTESIAN_POINT ( 'NONE',  ( -3.186695398571379290, -5.131874999999967990, 0.9679749472946410638 ) ) ;
#3921=CARTESIAN_POINT ( 'NONE',  ( 1.514604053328734823, -3.187500000000060396, -3.660349086209866876 ) ) ;
#3923=CARTESIAN_POINT ( 'NONE',  ( -2.392265219297526002, -4.639838562373030051, 2.913436905822091028 ) ) ;
#3925=CARTESIAN_POINT ( 'NONE',  ( 3.359686712365983929, -1.506874999999983755, 1.796916873358819222 ) ) ;
#3931=CARTESIAN_POINT ( 'NONE',  ( 2.898929819200243063, -5.329854288497422488, 1.773108554050290442 ) ) ;
#3936=AXIS2_PLACEMENT_3D ( 'NONE', #13170, #12005, #3465 ) ;
#3937=ORIENTED_EDGE ( 'NONE', *, *, #12854, .T. ) ;
#3943=CARTESIAN_POINT ( 'NONE',  ( -3.586083906644842223, -3.069375000000151399, -0.3518610084925551384 ) ) ;
#3950=CARTESIAN_POINT ( 'NONE',  ( 2.088010756335936691, -0.4995676945082540010, -3.523544157046685221 ) ) ;
#3962=CARTESIAN_POINT ( 'NONE',  ( 3.503209385669602938, -1.647500000000019948, -1.450007420588620866 ) ) ;
#3963=CARTESIAN_POINT ( 'NONE',  ( 1.804739227294467563, -4.171875000000069278, -3.379404665904198968 ) ) ;
#3965=FACE_OUTER_BOUND ( 'NONE', #10527, .T. ) ;
#3966=CARTESIAN_POINT ( 'NONE',  ( -4.991962918341529054, 1.883037081658660572, -0.3536665959326726338 ) ) ;
#3968=LINE ( 'NONE', #7475, #12266 ) ;
#3975=VERTEX_POINT ( 'NONE', #551 ) ;
#3976=CARTESIAN_POINT ( 'NONE',  ( 0.9404171202241153882, -5.788124999999990195, -3.104336352551608336 ) ) ;
#3978=CARTESIAN_POINT ( 'NONE',  ( -0.001216256839607751574, -5.834999999999983977, -3.237452472516329838 ) ) ;
#3987=CARTESIAN_POINT ( 'NONE',  ( 3.803621785104590794E-17, 9.355654565435173708, 0.000000000000000000 ) ) ;
#3991=CARTESIAN_POINT ( 'NONE',  ( -2.876356209513419415, -2.375000000000007994, -2.877876508394843658 ) ) ;
#3993=CARTESIAN_POINT ( 'NONE',  ( -1.836186059027842044, -3.671088562373069131, 3.438281954767565374 ) ) ;
#3996=EDGE_CURVE ( 'NONE', #5763, #2643, #5297, .T. ) ;
#3997=CARTESIAN_POINT ( 'NONE',  ( 9.531855622864829864E-16, 8.384405323238834029, 0.000000000000000000 ) ) ;
#4000=EDGE_CURVE ( 'NONE', #4411, #10656, #3968, .T. ) ;
#4012=CARTESIAN_POINT ( 'NONE',  ( -1.090659875871101692, -1.881874999999897602, -3.598793876473022735 ) ) ;
#4024=DIRECTION ( 'NONE',  ( -2.551930889570659960E-15, 1.000000000000000000, 0.000000000000000000 ) ) ;
#4029=ORIENTED_EDGE ( 'NONE', *, *, #10366, .F. ) ;
#4034=VERTEX_POINT ( 'NONE', #10150 ) ;
#4038=CARTESIAN_POINT ( 'NONE',  ( -3.566427039428707868, -2.131875000000089670, 1.083295335393480219 ) ) ;
#4042=CARTESIAN_POINT ( 'NONE',  ( -2.784563489868539410, -3.375000000000053735, -2.782533402055042071 ) ) ;
#4044=CARTESIAN_POINT ( 'NONE',  ( 1.732658076282644233, 0.04645217140506596037, 4.500000000000000000 ) ) ;
#4047=CARTESIAN_POINT ( 'NONE',  ( -3.008642795497751266, 2.054436331234726687, -3.788877816371842844 ) ) ;
#4048=CARTESIAN_POINT ( 'NONE',  ( -3.998008487304611336, -1.546875000000091038, 1.214361949261595131 ) ) ;
#4049=CARTESIAN_POINT ( 'NONE',  ( -2.598076211353320453, 2.374999999999993339, 4.500000000000000888 ) ) ;
#4068=CARTESIAN_POINT ( 'NONE',  ( 1.916065064279496746E-15, 7.362499999999997158, 0.000000000000000000 ) ) ;
#4077=CARTESIAN_POINT ( 'NONE',  ( -1.898222722261231343, -2.671874999999975131, 3.554431989243950873 ) ) ;
#4091=( NAMED_UNIT ( * ) SI_UNIT ( $, .STERADIAN. ) SOLID_ANGLE_UNIT ( ) );
#4094=CARTESIAN_POINT ( 'NONE',  ( 2.926652851519856213, -1.694375000000067022, -2.400566300852225776 ) ) ;
#4100=CARTESIAN_POINT ( 'NONE',  ( 1.453141968011759877, -5.138246789499178568, -3.363386372659848966 ) ) ;
#4103=CARTESIAN_POINT ( 'NONE',  ( 0.3070149676124478977, -0.4995676945082583309, -4.130607965512141710 ) ) ;
#4113=EDGE_LOOP ( 'NONE', ( #4321, #8157, #13567, #14612, #6699 ) ) ;
#4121=CARTESIAN_POINT ( 'NONE',  ( 3.730555813499059070, -1.553749999999926246, 0.7430650243616524486 ) ) ;
#4122=CARTESIAN_POINT ( 'NONE',  ( -3.331846864947428877, -4.578125000000028422, 1.779793940175935729 ) ) ;
#4126=CARTESIAN_POINT ( 'NONE',  ( -3.490494984142799684, -1.406250000000081268, -2.330449509171077516 ) ) ;
#4134=AXIS2_PLACEMENT_3D ( 'NONE', #10025, #3047, #5463 ) ;
#4144=CARTESIAN_POINT ( 'NONE',  ( -1.520556115814812870, -5.913125000000218456, -2.846480943363819183 ) ) ;
#4152=CARTESIAN_POINT ( 'NONE',  ( 1.903042727507366250, -4.428749999999965326, 2.845810502761935368 ) ) ;
#4159=CARTESIAN_POINT ( 'NONE',  ( 4.118464008547413790, -2.000000000000003109, 0.001090570402295849319 ) ) ;
#4161=CARTESIAN_POINT ( 'NONE',  ( 1.125729777374074869, -3.796088562373163722, 3.714534500553497764 ) ) ;
#4164=AXIS2_PLACEMENT_3D ( 'NONE', #82, #12982, #13137 ) ;
#4167=CARTESIAN_POINT ( 'NONE',  ( 2.931404194366990623, 4.650702586819546624, 3.589934763638662607E-16 ) ) ;
#4175=CARTESIAN_POINT ( 'NONE',  ( -0.7236788045118249801, -2.303749999999964437, 3.633254187536902879 ) ) ;
#4194=CARTESIAN_POINT ( 'NONE',  ( 3.570415799723221095, -6.014838562373082453, -0.3529878125807653366 ) ) ;
#4196=CARTESIAN_POINT ( 'NONE',  ( -3.756875241620029282, -3.453125000000005773, -1.140712293363390861 ) ) ;
#4201=CARTESIAN_POINT ( 'NONE',  ( 4.172905853428635403, -0.9687499999999248379, 0.8311981373062848899 ) ) ;
#4206=ORIENTED_EDGE ( 'NONE', *, *, #1576, .T. ) ;
#4207=CARTESIAN_POINT ( 'NONE',  ( -1.629699455448989389E-14, 8.699999999999999289, 5.655858585055787181E-29 ) ) ;
#4212=CARTESIAN_POINT ( 'NONE',  ( -1.864549691619314498, -4.928749999999819664, -2.792029179168366237 ) ) ;
#4218=CARTESIAN_POINT ( 'NONE',  ( 1.213339409441202221, -0.4995676945082561660, 3.847960304831221645 ) ) ;
#4228=CARTESIAN_POINT ( 'NONE',  ( 1.536269025742735383, -2.812500000000037303, 3.705069426614713723 ) ) ;
#4237=CARTESIAN_POINT ( 'NONE',  ( -2.598076211353319120, 1.678847577293364424, 4.500000000000000888 ) ) ;
#4238=CARTESIAN_POINT ( 'NONE',  ( -3.897114317029974462, -9.945166405816860437E-15, 2.249999999999999112 ) ) ;
#4244=CARTESIAN_POINT ( 'NONE',  ( -0.3768771888558096750, -1.319375000000004405, 3.816279424444235513 ) ) ;
#4258=ORIENTED_EDGE ( 'NONE', *, *, #6345, .T. ) ;
#4259=ORIENTED_EDGE ( 'NONE', *, *, #8010, .T. ) ;
#4261=CARTESIAN_POINT ( 'NONE',  ( -3.263656433892394126, -6.436713562373405750, -1.350434304814589925 ) ) ;
#4263=CARTESIAN_POINT ( 'NONE',  ( -1.834300037444539511, -0.9131249999999379030, -3.428720741157346374 ) ) ;
#4265=CARTESIAN_POINT ( 'NONE',  ( 0.4056240317150583419, -1.765625000000045741, 4.129595427369183724 ) ) ;
#4266=DIRECTION ( 'NONE',  ( -1.000000000000000000, 0.000000000000000000, 0.000000000000000000 ) ) ;
#4274=PRODUCT_DEFINITION_FORMATION_WITH_SPECIFIED_SOURCE ( 'ANY', '', #9565, .NOT_KNOWN. ) ;
#4290=CARTESIAN_POINT ( 'NONE',  ( 2.919796888921922573, -5.104126807837104707, -2.256669152708658643 ) ) ;
#4293=CIRCLE ( 'NONE', #2300, 0.5000000000000000000 ) ;
#4294=CARTESIAN_POINT ( 'NONE',  ( -3.090028468548657425, -5.022500000000056808, -1.280849571915205765 ) ) ;
#4300=VECTOR ( 'NONE', #2154, 999.9999999999998863 ) ;
#4301=CARTESIAN_POINT ( 'NONE',  ( -3.324804228637022074, -0.6093749999999287237, 2.730601746129839746 ) ) ;
#4320=CARTESIAN_POINT ( 'NONE',  ( 2.949251946438324889, -1.475624999999980647, 2.418581166398251714 ) ) ;
#4321=ORIENTED_EDGE ( 'NONE', *, *, #12659, .F. ) ;
#4322=VECTOR ( 'NONE', #10920, 1000.000000000000000 ) ;
#4325=ADVANCED_FACE ( 'NONE', ( #6448 ), #1131, .T. ) ;
#4341=CARTESIAN_POINT ( 'NONE',  ( 1.242853247313903786, -5.772499999999809006, -2.998378529913433788 ) ) ;
#4345=CARTESIAN_POINT ( 'NONE',  ( -0.7085372255082872384, -5.717963562373346242, 3.557256890250359849 ) ) ;
#4346=CARTESIAN_POINT ( 'NONE',  ( -1.113040416940756172, -1.288124999999980425, 3.674042195187707360 ) ) ;
#4349=CARTESIAN_POINT ( 'NONE',  ( 3.968938162104017842, -2.984375000000153211, 0.3919611025626033030 ) ) ;
#4358=MECHANICAL_DESIGN_GEOMETRIC_PRESENTATION_REPRESENTATION('',(#6609),#7592);
#4364=CARTESIAN_POINT ( 'NONE',  ( 2.619799856955864925, -4.694374999999869402, -2.148899555557211904 ) ) ;
#4371=CARTESIAN_POINT ( 'NONE',  ( 2.377331891390069174, -0.4995676945082533349, 3.200807742935684264 ) ) ;
#4382=CARTESIAN_POINT ( 'NONE',  ( -1.962865815818235271, -1.671875000000012879, 3.669921287786785502 ) ) ;
#4384=CARTESIAN_POINT ( 'NONE',  ( 0.7848530992743523171, -2.780463562373096664, 3.938237677807348902 ) ) ;
#4393=CARTESIAN_POINT ( 'NONE',  ( -1.673688575075004152E-15, 4.650702586819541295, 0.000000000000000000 ) ) ;
#4396=CARTESIAN_POINT ( 'NONE',  ( -0.7729260235471412388, -0.3037499999998679590, 3.893172034236696444 ) ) ;
#4400=CARTESIAN_POINT ( 'NONE',  ( 1.779210140229128934, -1.756874999999983755, -3.331607052712222572 ) ) ;
#4411=VERTEX_POINT ( 'NONE', #380 ) ;
#4420=CARTESIAN_POINT ( 'NONE',  ( 3.756292859848789689, -0.6318749999998841682, -1.140955529460117690 ) ) ;
#4423=CARTESIAN_POINT ( 'NONE',  ( 3.414669715040141273, -2.093749999999965805, -2.280302418758094252 ) ) ;
#4427=CARTESIAN_POINT ( 'NONE',  ( 4.991962918341520172, 1.883037081658684775, 0.3536665959326708575 ) ) ;
#4439=CARTESIAN_POINT ( 'NONE',  ( 0.6686498792469546260, -4.366249999999815223, 3.366016213005436075 ) ) ;
#4440=B_SPLINE_CURVE_WITH_KNOTS ( 'NONE', 3,
 ( #9120, #3227, #13859, #2216 ),
 .UNSPECIFIED., .F., .F.,
 ( 4, 4 ),
 ( 0.004347030683767774163, 0.006950528372497996078 ),
 .UNSPECIFIED. ) ;
#4443=CARTESIAN_POINT ( 'NONE',  ( -6.060835862730317059E-15, 2.375000000000000000, 0.000000000000000000 ) ) ;
#4446=CARTESIAN_POINT ( 'NONE',  ( -2.028590488616179410, -0.4995676945082638820, 3.621854581741517531 ) ) ;
#4448=SHAPE_REPRESENTATION ( 'Self-Tapping Grease Fitting_8742T12', ( #285 ), #8480 ) ;
#4455=CARTESIAN_POINT ( 'NONE',  ( -3.980019242547642833, -0.5625000000000109912, 1.650257999534034514 ) ) ;
#4457=CARTESIAN_POINT ( 'NONE',  ( 3.798302739331970379, -2.061713562373112651, -1.572130684568777692 ) ) ;
#4463=CARTESIAN_POINT ( 'NONE',  ( 3.250000000000017764, 7.362500000000000711, 0.000000000000000000 ) ) ;
#4464=PLANE ( 'NONE',  #7255 ) ;
#4467=CARTESIAN_POINT ( 'NONE',  ( 3.430119610663647567, -5.062500000000104805, -1.422280051980938431 ) ) ;
#4470=CARTESIAN_POINT ( 'NONE',  ( 3.601230736643932673, -2.553749999999958220, 0.7149504581460995878 ) ) ;
#4477=CONICAL_SURFACE ( 'NONE', #13417, 4.500000000000000888, 1.396263401595466691 ) ;
#4482=CARTESIAN_POINT ( 'NONE',  ( 0.9808155824294417791, -4.788124999999903153, -3.230360883553722307 ) ) ;
#4487=AXIS2_PLACEMENT_3D ( 'NONE', #12311, #9960, #1901 ) ;
#4488=CARTESIAN_POINT ( 'NONE',  ( -1.671015529475609052, -6.327338562373312492, -3.128183168801260461 ) ) ;
#4489=CARTESIAN_POINT ( 'NONE',  ( -1.153796164589722117, -0.2881249999999724309, 3.799958344797442766 ) ) ;
#4493=CARTESIAN_POINT ( 'NONE',  ( 1.953452353076893244, -1.828124999999917399, 3.651470988527475647 ) ) ;
#4496=CARTESIAN_POINT ( 'NONE',  ( 3.440513747128896682, 2.288586792248404223, 3.040855385833559854 ) ) ;
#4497=DIRECTION ( 'NONE',  ( -9.422394424380278809E-16, 1.000000000000000000, -0.000000000000000000 ) ) ;
#4512=CARTESIAN_POINT ( 'NONE',  ( -3.406603204915101379, -4.053749999999936016, -0.6763000812039869913 ) ) ;
#4518=CARTESIAN_POINT ( 'NONE',  ( -0.4546285099643554983, 2.357490090282483131, -4.499999999999999112 ) ) ;
#4530=CARTESIAN_POINT ( 'NONE',  ( -3.468190155366909888, -1.593749999999917621, 2.319185894079683230 ) ) ;
#4531=ORIENTED_EDGE ( 'NONE', *, *, #6717, .F. ) ;
#4533=CARTESIAN_POINT ( 'NONE',  ( -4.052888063889493964, -2.499213562373234776, 0.001471977874382501914 ) ) ;
#4546=CARTESIAN_POINT ( 'NONE',  ( 2.054976948924152946, -5.156250000000162537, -3.077941148907540558 ) ) ;
#4548=CARTESIAN_POINT ( 'NONE',  ( 2.024885806073651651, -2.741249999999974207, -3.032875982375832891 ) ) ;
#4563=ORIENTED_EDGE ( 'NONE', *, *, #9425, .T. ) ;
#4568=CARTESIAN_POINT ( 'NONE',  ( 1.764499024435270735, -4.827338562373064690, 3.303210492129881715 ) ) ;
#4569=CARTESIAN_POINT ( 'NONE',  ( 3.258191480560199693, -0.6787499999999294653, -2.178773987163739267 ) ) ;
#4570=CARTESIAN_POINT ( 'NONE',  ( -3.970076885172157066, -2.531249999999920064, 0.7911966920917139490 ) ) ;
#4573=CARTESIAN_POINT ( 'NONE',  ( -4.353714886931050465, 2.288586792248385571, 1.459144614166439036 ) ) ;
#4579=CARTESIAN_POINT ( 'NONE',  ( -1.287538504858034338, -4.897500000000167830, -3.105113058795574421 ) ) ;
#4589=CARTESIAN_POINT ( 'NONE',  ( 2.991299100910195019, -4.663125000000096776, -1.600316903339956243 ) ) ;
#4592=CARTESIAN_POINT ( 'NONE',  ( 3.031088913245534755, 0.04639863247564005727, 3.749999999999998668 ) ) ;
#4595=DIRECTION ( 'NONE',  ( -1.000000000000000000, 0.000000000000000000, 0.000000000000000000 ) ) ;
#4610=CARTESIAN_POINT ( 'NONE',  ( -1.590481721991226172, -1.687500000000021760, 3.843696589995393875 ) ) ;
#4613=CARTESIAN_POINT ( 'NONE',  ( 3.820744039781721391, -2.952338562373035380, 1.160108555621480519 ) ) ;
#4616=CIRCLE ( 'NONE', #14993, 2.093999815491831562 ) ;
#4625=CARTESIAN_POINT ( 'NONE',  ( 3.557408335254829801, -5.205290677742872241, -0.3931923741407351014 ) ) ;
#4632=CARTESIAN_POINT ( 'NONE',  ( -3.916933349122203367, -0.1162499999999876271, 0.7806084585172713419 ) ) ;
#4633=VERTEX_POINT ( 'NONE', #4642 ) ;
#4635=CARTESIAN_POINT ( 'NONE',  ( 0.3573659033054957801, -2.819374999999921805, -3.618812876704415427 ) ) ;
#4637=CIRCLE ( 'NONE', #7375, 0.8000000000000052625 ) ;
#4642=CARTESIAN_POINT ( 'NONE',  ( -2.514916625122314731, 4.927357795815630048, 0.000000000000000000 ) ) ;
#4650=CARTESIAN_POINT ( 'NONE',  ( -3.468991550463838891, -4.085000000000062137, -0.0008868951686453910126 ) ) ;
#4654=CARTESIAN_POINT ( 'NONE',  ( -2.916346042413609840, -4.608588562373151731, 2.395174355888781026 ) ) ;
#4664=CARTESIAN_POINT ( 'NONE',  ( 3.384491019838401726, -4.600625000000129639, -0.3324735777645301260 ) ) ;
#4667=DIRECTION ( 'NONE',  ( -9.422394424380278809E-16, 1.000000000000000000, -0.000000000000000000 ) ) ;
#4671=CONICAL_SURFACE ( 'NONE', #2933, 3.250000000000015987, 0.4363323129985828275 ) ;
#4675=CARTESIAN_POINT ( 'NONE',  ( -0.6956252696767697419, -3.303750000000123421, 3.503916970779588969 ) ) ;
#4685=AXIS2_PLACEMENT_3D ( 'NONE', #12168, #9909, #8674 ) ;
#4690=CARTESIAN_POINT ( 'NONE',  ( 0.8505843571400346637, -0.2187500000000167921, -4.270207479395898176 ) ) ;
#4692=ADVANCED_FACE ( 'NONE', ( #15089 ), #2128, .T. ) ;
#4693=CARTESIAN_POINT ( 'NONE',  ( 0.3927583221442342287, -2.764838562373139741, 3.998546384597275516 ) ) ;
#4698=CARTESIAN_POINT ( 'NONE',  ( 4.130341191321588390, 2.356280171323994921, -1.846039204036428849 ) ) ;
#4706=CARTESIAN_POINT ( 'NONE',  ( 3.837491448225466062, -3.984374999999830802, 0.3765428855677108166 ) ) ;
#4709=CARTESIAN_POINT ( 'NONE',  ( -2.355664480073890399, -2.225624999999979092, 2.872538697791624518 ) ) ;
#4713=DIRECTION ( 'NONE',  ( -1.747085166004344019E-15, 1.000000000000000000, -0.000000000000000000 ) ) ;
#4714=DIRECTION ( 'NONE',  ( -2.551930889570659960E-15, 1.000000000000000000, 0.000000000000000000 ) ) ;
#4722=CARTESIAN_POINT ( 'NONE',  ( 2.642398951855386979, -4.475625000000026610, 2.166914421091104881 ) ) ;
#4726=CARTESIAN_POINT ( 'NONE',  ( 3.694831845485670119, -3.952338562372989195, 1.119339768987546169 ) ) ;
#4728=DIRECTION ( 'NONE',  ( 0.8660254037844387076, 2.210036979070412685E-15, 0.4999999999999999445 ) ) ;
#4734=CARTESIAN_POINT ( 'NONE',  ( 1.656526992905777318, -3.756875000000012399, -3.097233728230734062 ) ) ;
#4749=DIRECTION ( 'NONE',  ( 0.7071067811865505703, -0.7071067811865444641, -8.659560562354948882E-17 ) ) ;
#4752=CARTESIAN_POINT ( 'NONE',  ( -2.598076211353319565, 1.678847577293365978, -4.499999999999999112 ) ) ;
#4754=AXIS2_PLACEMENT_3D ( 'NONE', #1110, #14138, #15296 ) ;
#4757=AXIS2_PLACEMENT_3D ( 'NONE', #13866, #12939, #8279 ) ;
#4764=CARTESIAN_POINT ( 'NONE',  ( -4.425813417735612987, 0.4843740197764026534, 0.4347324592064809035 ) ) ;
#4766=CARTESIAN_POINT ( 'NONE',  ( 1.616006145108879855, -1.186713562373049813, -3.905372697150129468 ) ) ;
#4779=CARTESIAN_POINT ( 'NONE',  ( 0.3668491701747067513, -4.765624999999817923, 3.734637934618871391 ) ) ;
#4782=CARTESIAN_POINT ( 'NONE',  ( -3.865847815970003154, -1.085000000000063469, -0.001011349278461548453 ) ) ;
#4784=CARTESIAN_POINT ( 'NONE',  ( -1.578751687972824502, -5.349924609423814204, 2.979769298184874682 ) ) ;
#4788=DIRECTION ( 'NONE',  ( -1.747085166004344019E-15, 1.000000000000000000, -0.000000000000000000 ) ) ;
#4791=CARTESIAN_POINT ( 'NONE',  ( 2.517719788909356549, -5.362458399163725353, 2.218656285138580486 ) ) ;
#4801=CARTESIAN_POINT ( 'NONE',  ( -1.054465238365617452, -2.881875000000049702, -3.471494129216006197 ) ) ;
#4818=CARTESIAN_POINT ( 'NONE',  ( -0.6836773592642079178, -3.866249999999994635, -3.430425219284937821 ) ) ;
#4828=CARTESIAN_POINT ( 'NONE',  ( -0.7073002561900942897, -2.866249999999988418, -3.560643744722076232 ) ) ;
#4831=CARTESIAN_POINT ( 'NONE',  ( 2.598076211353309350, 2.375000000000006661, 4.500000000000000000 ) ) ;
#4843=ORIENTED_EDGE ( 'NONE', *, *, #14162, .T. ) ;
#4846=CARTESIAN_POINT ( 'NONE',  ( 2.793566534610028018, 0.1406250000000374423, 3.401478000866359430 ) ) ;
#4848=CARTESIAN_POINT ( 'NONE',  ( -1.205651417374353773, -1.702338562373074904, 3.979684766797042528 ) ) ;
#4864=CARTESIAN_POINT ( 'NONE',  ( -2.475833455637627800, -3.640624999999937383, 3.015200003105952042 ) ) ;
#4868=CARTESIAN_POINT ( 'NONE',  ( 3.402892030661166523, -0.5020034630054815983, 1.955069923487531947 ) ) ;
#4870=CARTESIAN_POINT ( 'NONE',  ( -2.636171414473165608, -5.322656474840649743, 2.174809469211999691 ) ) ;
#4871=CIRCLE ( 'NONE', #1149, 2.093999815491831562 ) ;
#4875=FACE_OUTER_BOUND ( 'NONE', #11772, .T. ) ;
#4883=PRODUCT_DEFINITION_SHAPE ( 'NONE', 'NONE',  #3235 ) ;
#4885=CARTESIAN_POINT ( 'NONE',  ( 3.667419683216787352, -2.585000000000003517, 0.0009491222189902254192 ) ) ;
#4892=EDGE_CURVE ( 'NONE', #9382, #1688, #4616, .T. ) ;
#4900=CARTESIAN_POINT ( 'NONE',  ( -3.527726845254099075, -3.116249999999919140, 0.7030635791094290710 ) ) ;
#4912=CARTESIAN_POINT ( 'NONE',  ( 3.430119610663647567, -5.062500000000104805, -1.422280051980938431 ) ) ;
#4923=VERTEX_POINT ( 'NONE', #13703 ) ;
#4927=CARTESIAN_POINT ( 'NONE',  ( 3.398568864256001909, 0.1093749999999974742, 2.790657398000633727 ) ) ;
#4928=CARTESIAN_POINT ( 'NONE',  ( -1.984936106024998814, -1.327338562373031383, -3.710328542583766431 ) ) ;
#4939=CARTESIAN_POINT ( 'NONE',  ( -3.018109139697564114, -3.609375000000057732, 2.478742592228960095 ) ) ;
#4942=CARTESIAN_POINT ( 'NONE',  ( -3.705025434593251177, -1.038125000000020393, -1.124966067554165727 ) ) ;
#4953=ORIENTED_EDGE ( 'NONE', *, *, #2607, .F. ) ;
#4955=CARTESIAN_POINT ( 'NONE',  ( 3.376561219002149894, -3.631875000000035048, -1.025635141340162315 ) ) ;
#4959=EDGE_LOOP ( 'NONE', ( #14967, #11198, #12789, #1296 ) ) ;
#4967=CARTESIAN_POINT ( 'NONE',  ( -0.3378546177656944205, -4.319374999999974207, 3.421346328963575711 ) ) ;
#4970=CARTESIAN_POINT ( 'NONE',  ( -2.577850803773733546, 4.297149196226267343, 0.000000000000000000 ) ) ;
#4976=EDGE_CURVE ( 'NONE', #2643, #7102, #9207, .T. ) ;
#4977=CARTESIAN_POINT ( 'NONE',  ( 3.463329978863818770, -3.616249999999970210, -0.6879750677194342856 ) ) ;
#4984=DIRECTION ( 'NONE',  ( 0.7933533402912347210, 0.6087614290087212110, 9.715776287805233806E-17 ) ) ;
#4988=CARTESIAN_POINT ( 'NONE',  ( 0.8000000000000193623, -5.500000000000000888, 9.797174393179008575E-17 ) ) ;
#4993=CARTESIAN_POINT ( 'NONE',  ( 1.553520276525308219, -5.413125000000014175, 2.903814772855817239 ) ) ;
#4995=CARTESIAN_POINT ( 'NONE',  ( 3.655516518246672231, 0.09375000000004835021, 2.440638533248514541 ) ) ;
#4996=EDGE_CURVE ( 'NONE', #4633, #5205, #2378, .T. ) ;
#4997=CARTESIAN_POINT ( 'NONE',  ( 0.4212773118942713668, -0.7648385623731170924, 4.261548716872522569 ) ) ;
#4998=CIRCLE ( 'NONE', #1263, 0.5000000000000000000 ) ;
#5009=ORIENTED_EDGE ( 'NONE', *, *, #9425, .F. ) ;
#5012=CARTESIAN_POINT ( 'NONE',  ( -2.784563489868539410, -3.375000000000053735, -2.782533402055042071 ) ) ;
#5015=CARTESIAN_POINT ( 'NONE',  ( -3.619583526789921457, -4.546088562373016728, 1.096959227905920597 ) ) ;
#5016=CARTESIAN_POINT ( 'NONE',  ( 0.001402937982463629916, -1.335000000000034825, 3.832736870811212171 ) ) ;
#5017=CARTESIAN_POINT ( 'NONE',  ( -3.412320100379302446, -5.286939238114719330, 0.5937987388295963287 ) ) ;
#5030=CARTESIAN_POINT ( 'NONE',  ( 2.928286698324767734, -3.678750000000110987, -1.958188979435659283 ) ) ;
#5040=CARTESIAN_POINT ( 'NONE',  ( -4.287904177287694907, -0.4995676945082599407, -0.3292842791088227417 ) ) ;
#5054=CARTESIAN_POINT ( 'NONE',  ( 1.779210140229128934, -1.756874999999983755, -3.331607052712222572 ) ) ;
#5055=CARTESIAN_POINT ( 'NONE',  ( 3.775473633219732505, -4.031249999999629630, -0.7524242524445519109 ) ) ;
#5071=CARTESIAN_POINT ( 'NONE',  ( -0.9391448502757393513, -5.881874999999767262, -3.091762488354312222 ) ) ;
#5075=DIRECTION ( 'NONE',  ( -1.000000000000000000, -1.783664229908549233E-15, 0.000000000000000000 ) ) ;
#5076=B_SPLINE_CURVE_WITH_KNOTS ( 'NONE', 3,
 ( #4237, #14780, #13631, #663, #13478, #7734, #2843, #511, #12462, #8963, #1826, #5416, #10117, #13701 ),
 .UNSPECIFIED., .F., .F.,
 ( 4, 2, 2, 2, 2, 2, 4 ),
 ( 0.004061142180336881069, 0.005409079593014973729, 0.006083048299354019625, 0.006757017005693066389, 0.008104954418371158181, 0.008778923124710204945, 0.009452891831049249974 ),
 .UNSPECIFIED. ) ;
#5077=CARTESIAN_POINT ( 'NONE',  ( 4.074635740569324760, -0.9523385623730679095, 1.234421966825711481 ) ) ;
#5091=SURFACE_STYLE_USAGE ( .BOTH. , #10981 ) ;
#5093=CARTESIAN_POINT ( 'NONE',  ( -1.920019182618211584, -2.328124999999937383, -3.594387849940205104 ) ) ;
#5097=CARTESIAN_POINT ( 'NONE',  ( 2.619318502887032718, -5.124213562373151731, -2.621246189942336713 ) ) ;
#5098=AXIS2_PLACEMENT_3D ( 'NONE', #10876, #8846, #9141 ) ;
#5099=VECTOR ( 'NONE', #8622, 1000.000000000000000 ) ;
#5100=CARTESIAN_POINT ( 'NONE',  ( 3.915012698312653860, -0.5693749999999865308, 0.3866328316385073127 ) ) ;
#5117=CARTESIAN_POINT ( 'NONE',  ( 2.337649614532406162, -2.444375000000051479, 2.849939602875970035 ) ) ;
#5135=ORIENTED_EDGE ( 'NONE', *, *, #3354, .F. ) ;
#5139=CARTESIAN_POINT ( 'NONE',  ( -2.629016928070645243, -2.210000000000078568, 2.627652665972809665 ) ) ;
#5141=VECTOR ( 'NONE', #10350, 1000.000000000000000 ) ;
#5142=CARTESIAN_POINT ( 'NONE',  ( 0.7730394778201963302, -3.218749999999914735, -3.881000975522858720 ) ) ;
#5146=FACE_OUTER_BOUND ( 'NONE', #12570, .T. ) ;
#5156=CARTESIAN_POINT ( 'NONE',  ( 1.804507757947518609, -5.741250000000162501, -2.702832914148806776 ) ) ;
#5160=CARTESIAN_POINT ( 'NONE',  ( -1.266249875242109413, -5.272499999999733511, 3.060236832100306614 ) ) ;
#5164=ADVANCED_BREP_SHAPE_REPRESENTATION ( '', ( #442, #285 ), #8480 ) ;
#5167=CARTESIAN_POINT ( 'NONE',  ( -2.093999815491831562, 9.499999999999998224, 2.703148537761814673E-16 ) ) ;
#5172=CARTESIAN_POINT ( 'NONE',  ( 3.414669715040141273, -2.093749999999965805, -2.280302418758094252 ) ) ;
#5174=EDGE_CURVE ( 'NONE', #11015, #12263, #12064, .T. ) ;
#5191=CARTESIAN_POINT ( 'NONE',  ( -1.113040416940732857, -1.288124999999980425, 3.674042195187707804 ) ) ;
#5196=CARTESIAN_POINT ( 'NONE',  ( 0.3693243909029986227, -5.159404925397325314, -3.617482621258250486 ) ) ;
#5202=EDGE_LOOP ( 'NONE', ( #15335, #2969 ) ) ;
#5205=VERTEX_POINT ( 'NONE', #5621 ) ;
#5210=CARTESIAN_POINT ( 'NONE',  ( 1.412068586280907923, -2.397499999999971099, 3.411535633775557574 ) ) ;
#5211=CARTESIAN_POINT ( 'NONE',  ( -2.165165973034034685, -3.656250000000003997, 3.242962682996374912 ) ) ;
#5221=LINE ( 'NONE', #2892, #13716 ) ;
#5223=ORIENTED_EDGE ( 'NONE', *, *, #14711, .T. ) ;
#5224=CARTESIAN_POINT ( 'NONE',  ( -2.589953986283602294, -4.975625000000236220, -2.126619835350849641 ) ) ;
#5236=ADVANCED_FACE ( 'NONE', ( #2106 ), #9561, .T. ) ;
#5238=CIRCLE ( 'NONE', #4487, 4.401041666666736241 ) ;
#5240=CARTESIAN_POINT ( 'NONE',  ( 0.3952026422296860964, -2.765624999999906741, 3.997656568947202338 ) ) ;
#5245=CARTESIAN_POINT ( 'NONE',  ( 0.8000000000000113687, 9.500000000000000000, 9.797174393178965434E-17 ) ) ;
#5250=CARTESIAN_POINT ( 'NONE',  ( -9.797174393178965434E-17, 9.500000000000000000, 0.000000000000000000 ) ) ;
#5252=DIRECTION ( 'NONE',  ( 2.551930889570659960E-15, -1.000000000000000000, -0.000000000000000000 ) ) ;
#5259=CARTESIAN_POINT ( 'NONE',  ( -2.976231983981254992, -1.194374999999927578, 2.444352914378568276 ) ) ;
#5263=B_SPLINE_CURVE_WITH_KNOTS ( 'NONE', 3,
 ( #3347, #9161, #4592, #13899 ),
 .UNSPECIFIED., .F., .F.,
 ( 4, 4 ),
 ( 0.002598307151460991539, 0.005196383362814307842 ),
 .UNSPECIFIED. ) ;
#5274=EDGE_CURVE ( 'NONE', #8682, #11015, #2019, .T. ) ;
#5288=CARTESIAN_POINT ( 'NONE',  ( 3.667419683216786908, -2.585000000000003517, 0.0009491222189788412963 ) ) ;
#5291=CARTESIAN_POINT ( 'NONE',  ( 2.712400463490634017, -4.125000000000058620, -2.714386550172725787 ) ) ;
#5294=CARTESIAN_POINT ( 'NONE',  ( -9.797174393178927223E-17, 9.500000000000000000, 0.000000000000000000 ) ) ;
#5296=CARTESIAN_POINT ( 'NONE',  ( -4.264150341155778179, -0.5211359837986738741, 0.5700929974395811950 ) ) ;
#5297=LINE ( 'NONE', #4049, #5099 ) ;
#5302=CARTESIAN_POINT ( 'NONE',  ( -4.330127018922192761, -1.133719399746323553E-14, 1.499999999999998002 ) ) ;
#5315=CARTESIAN_POINT ( 'NONE',  ( 0.5699749950174962665, -0.4995676945082574427, 4.018060920292908733 ) ) ;
#5316=CARTESIAN_POINT ( 'NONE',  ( -0.9755776780686565841, -4.881874999999863185, -3.218989981404408951 ) ) ;
#5321=CARTESIAN_POINT ( 'NONE',  ( -0.7834809220335302582, -2.718750000000123013, 3.946322201046845279 ) ) ;
#5340=CARTESIAN_POINT ( 'NONE',  ( -1.750120246539717428, -2.256875000000012843, 3.272202384321438284 ) ) ;
#5348=VECTOR ( 'NONE', #111, 1000.000000000000000 ) ;
#5350=CARTESIAN_POINT ( 'NONE',  ( 3.897114317029974018, 9.945166405816858860E-15, -2.250000000000001332 ) ) ;
#5363=ORIENTED_EDGE ( 'NONE', *, *, #6678, .T. ) ;
#5367=CARTESIAN_POINT ( 'NONE',  ( 3.525223957706937306, -5.967963562373009623, 0.6998565464874195730 ) ) ;
#5369=CARTESIAN_POINT ( 'NONE',  ( 0.7224497989600745518, -2.366250000000003517, 3.625028471221638071 ) ) ;
#5373=CARTESIAN_POINT ( 'NONE',  ( 0.7565055315742956754, -3.781249999999899636, 3.808421443275634921 ) ) ;
#5376=CARTESIAN_POINT ( 'NONE',  ( -4.362044368365340929, -1.127570259384924611E-14, 0.000000000000000000 ) ) ;
#5377=CARTESIAN_POINT ( 'NONE',  ( -4.296274425956841725, -0.5002988223950231017, 0.02453012155904704325 ) ) ;
#5393=CARTESIAN_POINT ( 'NONE',  ( -3.336666538900096679, -5.084999999999988418, 0.001247370357366475637 ) ) ;
#5402=CARTESIAN_POINT ( 'NONE',  ( 1.454275362300765373, -5.407858183789424622, 2.950057805584367809 ) ) ;
#5406=ORIENTED_EDGE ( 'NONE', *, *, #10238, .T. ) ;
#5409=CARTESIAN_POINT ( 'NONE',  ( -1.859859099471618649, -3.328125000000058620, -3.476502332403788476 ) ) ;
#5416=CARTESIAN_POINT ( 'NONE',  ( 2.192040893916867184, 1.873195365144028290, 4.500000000000000888 ) ) ;
#5417=CARTESIAN_POINT ( 'NONE',  ( -3.031088913245534755, 0.04639863247562457660, 3.749999999999999556 ) ) ;
#5423=CARTESIAN_POINT ( 'NONE',  ( -1.834300037444539955, -0.9131249999999379030, -3.428720741157346819 ) ) ;
#5425=CARTESIAN_POINT ( 'NONE',  ( 2.598076211353310239, 1.678847577293378857, -4.499999999999999112 ) ) ;
#5434=B_SPLINE_CURVE_WITH_KNOTS ( 'NONE', 3,
 ( #7796, #7937, #1967, #14983 ),
 .UNSPECIFIED., .F., .F.,
 ( 4, 4 ),
 ( 0.7672515605989058685, 0.7674537633733152786 ),
 .UNSPECIFIED. ) ;
#5443=CARTESIAN_POINT ( 'NONE',  ( -3.640430666773472268, -5.483588562373210351, -0.3595019156637501712 ) ) ;
#5444=CARTESIAN_POINT ( 'NONE',  ( -3.516205069202310352, -0.1631249999999115075, 1.881096664271727059 ) ) ;
#5446=CARTESIAN_POINT ( 'NONE',  ( 1.584545095770156564, -1.812499999999970912, 3.828300384078624941 ) ) ;
#5450=CARTESIAN_POINT ( 'NONE',  ( -1.590481721991226172, -1.687500000000021760, 3.843696589995393875 ) ) ;
#5461=CARTESIAN_POINT ( 'NONE',  ( 3.333123593314366140, -4.616249999999967990, -0.6642911394208504960 ) ) ;
#5462=ADVANCED_FACE ( 'NONE', ( #1637, #10798 ), #13435, .F. ) ;
#5463=DIRECTION ( 'NONE',  ( 1.000000000000000000, 9.422394424380278809E-16, 0.000000000000000000 ) ) ;
#5468=CARTESIAN_POINT ( 'NONE',  ( 3.264569842716556369, -0.4995676945082427323, 2.204052319888019085 ) ) ;
#5471=CARTESIAN_POINT ( 'NONE',  ( -0.3227798623957894297, -5.319375000000161613, 3.289865787063878333 ) ) ;
#5476=ADVANCED_FACE ( 'NONE', ( #8458 ), #2615, .T. ) ;
#5481=CARTESIAN_POINT ( 'NONE',  ( 0.001544386136394801726, -0.7500000000000344169, 4.283781196144704317 ) ) ;
#5483=CARTESIAN_POINT ( 'NONE',  ( -3.899807011409266888, -3.514838562372941233, 0.3830646067729001625 ) ) ;
#5487=ADVANCED_FACE ( 'NONE', ( #5519 ), #12038, .T. ) ;
#5495=VECTOR ( 'NONE', #13989, 1000.000000000000000 ) ;
#5496=CARTESIAN_POINT ( 'NONE',  ( -3.733522804429754594, -2.085000000000140741, 0.001371824453763029108 ) ) ;
#5513=CARTESIAN_POINT ( 'NONE',  ( -2.103997734759340155, -5.225624999999808118, 2.565685703212198465 ) ) ;
#5514=VERTEX_POINT ( 'NONE', #2955 ) ;
#5517=CARTESIAN_POINT ( 'NONE',  ( 2.266335642362669045, -6.139838562372765374, -2.760089361353832427 ) ) ;
#5518=CARTESIAN_POINT ( 'NONE',  ( -2.976231983981160845, -1.194374999999927578, 2.444352914378567387 ) ) ;
#5519=FACE_OUTER_BOUND ( 'NONE', #10196, .T. ) ;
#5520=CARTESIAN_POINT ( 'NONE',  ( -2.240749814637992721, -2.656250000000047073, 3.351605112894145311 ) ) ;
#5526=CARTESIAN_POINT ( 'NONE',  ( -2.667636957649788698, -1.359375000000169198, -3.248130456407447575 ) ) ;
#5547=CARTESIAN_POINT ( 'NONE',  ( 3.372444421885775423, -0.4995676945082423992, 2.006840812041871924 ) ) ;
#5557=CARTESIAN_POINT ( 'NONE',  ( 3.016622086615760256, -0.8749999999999454880, 3.018230387793254810 ) ) ;
#5560=CARTESIAN_POINT ( 'NONE',  ( 4.043765020089121975, -1.967963562373018949, 0.8054683246621723303 ) ) ;
#5571=EDGE_CURVE ( 'NONE', #502, #11643, #7624, .T. ) ;
#5574=CARTESIAN_POINT ( 'NONE',  ( 3.084626646876158063, -5.093749999999860556, -2.059924370567768115 ) ) ;
#5579=CARTESIAN_POINT ( 'NONE',  ( 2.926652851519762955, -1.694375000000067022, -2.400566300852225776 ) ) ;
#5583=DIRECTION ( 'NONE',  ( -2.551930889570660354E-15, 1.000000000000000000, 0.000000000000000000 ) ) ;
#5584=CARTESIAN_POINT ( 'NONE',  ( 3.530157234965975555, -5.226201182446649440, -2.246195850846843811E-13 ) ) ;
#5592=CARTESIAN_POINT ( 'NONE',  ( -2.465526969817839031, -3.960000000000052811, -2.463696919997012014 ) ) ;
#5593=ORIENTED_EDGE ( 'NONE', *, *, #10869, .T. ) ;
#5596=CARTESIAN_POINT ( 'NONE',  ( -1.713569807928926991, -5.671088562373275188, 3.203872873516009800 ) ) ;
#5598=CARTESIAN_POINT ( 'NONE',  ( 3.639928100339127948, -0.5225000000000105116, 1.508827519571796172 ) ) ;
#5602=CARTESIAN_POINT ( 'NONE',  ( 1.567576417386008947, -2.187499999999996447, -3.781634774997608250 ) ) ;
#5606=CARTESIAN_POINT ( 'NONE',  ( -1.221455774822097329, -1.296874999999898082, -4.030457444822014956 ) ) ;
#5621=CARTESIAN_POINT ( 'NONE',  ( 2.514916625122327165, 4.927357795815638042, 3.529993346153717244E-16 ) ) ;
#5641=CARTESIAN_POINT ( 'NONE',  ( -4.238263498634291082, -0.4687499999999378830, -0.8414564874906409475 ) ) ;
#5643=CARTESIAN_POINT ( 'NONE',  ( 0.7964824889291316490, -2.217963562373153952, -4.011792787020751483 ) ) ;
#5650=EDGE_CURVE ( 'NONE', #1386, #11935, #11413, .T. ) ;
#5652=PRODUCT_CONTEXT ( 'NONE', #9108, 'mechanical' ) ;
#5655=CARTESIAN_POINT ( 'NONE',  ( -3.232499647488480399, -5.421874999999926281, -1.728882681842687452 ) ) ;
#5657=VECTOR ( 'NONE', #4749, 1000.000000000000114 ) ;
#5658=CARTESIAN_POINT ( 'NONE',  ( -1.054465238365572599, -2.881875000000049702, -3.471494129216005753 ) ) ;
#5661=FACE_OUTER_BOUND ( 'NONE', #12200, .T. ) ;
#5676=CARTESIAN_POINT ( 'NONE',  ( -0.3313405146687902203, -4.850625000000119869, -3.351331461923205080 ) ) ;
#5677=ORIENTED_EDGE ( 'NONE', *, *, #514, .F. ) ;
#5681=CARTESIAN_POINT ( 'NONE',  ( -3.978984329191358693, -0.08500000000000000611, -3.334211887901014441E-13 ) ) ;
#5684=CARTESIAN_POINT ( 'NONE',  ( 3.935506471057187206, -2.046874999999910738, -1.192685225358429912 ) ) ;
#5687=CARTESIAN_POINT ( 'NONE',  ( -4.296275033669348709, -0.4995676945082693776, 0.008185550287844470252 ) ) ;
#5696=CARTESIAN_POINT ( 'NONE',  ( 1.592243150387700146, -4.756875000000070131, -2.981552405995577359 ) ) ;
#5699=DIRECTION ( 'NONE',  ( 2.551930889570660354E-15, -1.000000000000000000, 0.000000000000000000 ) ) ;
#5701=CARTESIAN_POINT ( 'NONE',  ( -9.797174393178927223E-17, 9.500000000000000000, 0.000000000000000000 ) ) ;
#5710=CARTESIAN_POINT ( 'NONE',  ( -1.612261674935887568, -1.312500000000171863, -3.888369303904286589 ) ) ;
#5712=CARTESIAN_POINT ( 'NONE',  ( 2.899850257105391904, -2.124213562373065134, -2.901953948755849222 ) ) ;
#5724=CARTESIAN_POINT ( 'NONE',  ( -0.7178551545708362625, -5.281249999999999112, -3.613793911565672534 ) ) ;
#5727=CARTESIAN_POINT ( 'NONE',  ( -1.418005212499557466, -2.272500000000021281, 3.426931839692804349 ) ) ;
#5730=DIRECTION ( 'NONE',  ( -1.000000000000000000, -1.747085166004344019E-15, 0.000000000000000000 ) ) ;
#5731=CARTESIAN_POINT ( 'NONE',  ( 3.826752640285553397, -0.4995676945082493381, 1.002635565222667280 ) ) ;
#5740=CARTESIAN_POINT ( 'NONE',  ( 3.151910583997930004, -4.522499999999531894, 1.304188709559742643 ) ) ;
#5746=CARTESIAN_POINT ( 'NONE',  ( 3.654558516219509556, -4.967963562373524766, 0.7279234453325641452 ) ) ;
#5747=CARTESIAN_POINT ( 'NONE',  ( -3.865847815970003154, -1.085000000000063469, -0.001011349278461548453 ) ) ;
#5750=CARTESIAN_POINT ( 'NONE',  ( -2.876356209513419415, -2.375000000000007994, -2.877876508394843658 ) ) ;
#5763=VERTEX_POINT ( 'NONE', #13325 ) ;
#5766=CARTESIAN_POINT ( 'NONE',  ( 3.384491019838401726, -4.600625000000129639, -0.3324735777645301260 ) ) ;
#5768=CIRCLE ( 'NONE', #782, 0.2500000000000000000 ) ;
#5771=CARTESIAN_POINT ( 'NONE',  ( -1.120937138223994101, 2.242130364943868859, -4.499999999999998224 ) ) ;
#5777=AXIS2_PLACEMENT_3D ( 'NONE', #4443, #5699, #9162 ) ;
#5782=ORIENTED_EDGE ( 'NONE', *, *, #12108, .T. ) ;
#5784=CARTESIAN_POINT ( 'NONE',  ( 1.584545095770156564, -1.812499999999970912, 3.828300384078624941 ) ) ;
#5787=CARTESIAN_POINT ( 'NONE',  ( 3.675079574260619708, -3.061713562373090003, -1.523835802059044564 ) ) ;
#5799=ORIENTED_EDGE ( 'NONE', *, *, #7043, .F. ) ;
#5802=CARTESIAN_POINT ( 'NONE',  ( 1.415591119045080504, -5.187499999999808153, -3.415035020420910783 ) ) ;
#5805=CARTESIAN_POINT ( 'NONE',  ( -3.717546150574369879, -2.069374999999891607, -0.3671215460811757536 ) ) ;
#5820=ORIENTED_EDGE ( 'NONE', *, *, #7251, .T. ) ;
#5826=CARTESIAN_POINT ( 'NONE',  ( 1.807163061527332415, -4.171088562373018505, -3.378841529629734719 ) ) ;
#5838=CARTESIAN_POINT ( 'NONE',  ( 1.403561989263862998E-14, -5.500000000000001776, 0.000000000000000000 ) ) ;
#5839=EDGE_CURVE ( 'NONE', #4923, #3175, #11771, .T. ) ;
#5849=CARTESIAN_POINT ( 'NONE',  ( -3.581969766213484174, -3.100624999999847198, 0.3518610084922548231 ) ) ;
#5861=EDGE_LOOP ( 'NONE', ( #3021, #2305, #1260, #1490, #12769 ) ) ;
#5873=AXIS2_PLACEMENT_3D ( 'NONE', #14589, #702, #9930 ) ;
#5874=B_SPLINE_CURVE_WITH_KNOTS ( 'NONE', 3,
 ( #13495, #5040, #8904, #13645, #6374, #11088, #6222, #2861, #10930, #14489, #8605, #1542, #6297, #14714, #7608, #4103, #12331, #6446, #11157, #3950, #13418, #3877, #2708, #8830, #13575, #7452, #12698, #9125, #6740, #2070, #6820, #7896, #5731, #977, #6597, #13863 ),
 .UNSPECIFIED., .F., .F.,
 ( 4, 2, 2, 2, 2, 2, 2, 2, 2, 2, 2, 2, 2, 2, 2, 2, 2, 4 ),
 ( 0.000000000000000000, 0.0009396455755520615426, 0.001879291151104123085, 0.002818936726656184628, 0.003758582302208246170, 0.004698227877760306412, 0.005637873453312367521, 0.006577519028864427762, 0.007517164604416488871, 0.008456810179968549113, 0.009396455755520611089, 0.01033610133107267307, 0.01127574690662473504, 0.01221539248217679355, 0.01315503805772885379, 0.01362486084550488565, 0.01409468363328091750, 0.01503432920883297774 ),
 .UNSPECIFIED. ) ;
#5875=CARTESIAN_POINT ( 'NONE',  ( -3.751644922634416179, -2.436713562373012731, -1.555143193707982929 ) ) ;
#5890=CARTESIAN_POINT ( 'NONE',  ( 1.148200974759843618, -0.3818749999999526135, 3.788695824010691382 ) ) ;
#5893=CARTESIAN_POINT ( 'NONE',  ( 1.412068586280907923, -2.397499999999971099, 3.411535633775557574 ) ) ;
#5898=CARTESIAN_POINT ( 'NONE',  ( 0.8000000000000117018, 9.015594676761164550, 9.797174393178967899E-17 ) ) ;
#5911=CARTESIAN_POINT ( 'NONE',  ( 1.464250807817800482, -4.186713562373068243, -3.538677689569500906 ) ) ;
#5921=CARTESIAN_POINT ( 'NONE',  ( -0.3421672931279376995, -3.850625000000083009, -3.483230393025887661 ) ) ;
#5930=CARTESIAN_POINT ( 'NONE',  ( 2.315514200798038047, -2.725624999999891607, -2.819975302942780537 ) ) ;
#5949=CARTESIAN_POINT ( 'NONE',  ( 1.278996873743735163, 0.2031250000000478229, 4.220359392353129735 ) ) ;
#5952=CARTESIAN_POINT ( 'NONE',  ( -4.294764374624453040, -0.5148395451705815029, 0.4218660116795628356 ) ) ;
#5966=CARTESIAN_POINT ( 'NONE',  ( -3.160451915950723389, -4.406249999999939604, -2.110071460981538749 ) ) ;
#5981=CARTESIAN_POINT ( 'NONE',  ( -2.795825449145424191, -2.975624999999864517, -2.292747793747711427 ) ) ;
#5985=CARTESIAN_POINT ( 'NONE',  ( -0.3733708913937817675, -4.264838562373088671, -3.801067638221671263 ) ) ;
#5987=CARTESIAN_POINT ( 'NONE',  ( -3.897114317029974462, -9.945166405816860437E-15, 2.249999999999999112 ) ) ;
#5994=CARTESIAN_POINT ( 'NONE',  ( 2.255458548909140770, -3.444374999999939568, 2.746210667320699184 ) ) ;
#5996=ORIENTED_EDGE ( 'NONE', *, *, #1992, .T. ) ;
#6003=CARTESIAN_POINT ( 'NONE',  ( 1.974738715674944078, -3.428749999999933795, 2.957050713271639708 ) ) ;
#6015=AXIS2_PLACEMENT_3D ( 'NONE', #10729, #8474, #6183 ) ;
#6025=CARTESIAN_POINT ( 'NONE',  ( -2.461334822302656100, 0.3437500000001206257, 3.681509895155765655 ) ) ;
#6027=CARTESIAN_POINT ( 'NONE',  ( -3.189069343666966372, -6.084999999999998188, 0.000000000000000000 ) ) ;
#6042=CARTESIAN_POINT ( 'NONE',  ( 0.7565055315742956754, -3.781249999999899636, 3.808421443275634921 ) ) ;
#6047=CARTESIAN_POINT ( 'NONE',  ( 3.258191480560199693, -0.6787499999999294653, -2.178773987163739267 ) ) ;
#6052=DIRECTION ( 'NONE',  ( -1.000000000000000000, -2.551930889570659960E-15, 0.000000000000000000 ) ) ;
#6059=CARTESIAN_POINT ( 'NONE',  ( 3.463329978863732173, -3.616249999999970210, -0.6879750677194341746 ) ) ;
#6075=CARTESIAN_POINT ( 'NONE',  ( -1.685726645313963434, -3.256874999999974651, 3.156579729352138486 ) ) ;
#6080=ORIENTED_EDGE ( 'NONE', *, *, #1858, .T. ) ;
#6085=CARTESIAN_POINT ( 'NONE',  ( -0.0009180086920793713474, -3.334999999999859632, 3.568205616840286698 ) ) ;
#6089=CYLINDRICAL_SURFACE ( 'NONE', #13694, 0.8000000000000113687 ) ;
#6094=PLANE ( 'NONE',  #8323 ) ;
#6095=CARTESIAN_POINT ( 'NONE',  ( -1.006616814747114065E-29, -2.568816543514387226E-44, 0.000000000000000000 ) ) ;
#6103=FACE_OUTER_BOUND ( 'NONE', #3221, .T. ) ;
#6105=ORIENTED_EDGE ( 'NONE', *, *, #10376, .T. ) ;
#6106=CARTESIAN_POINT ( 'NONE',  ( 1.951466014313916641, -1.827338562372905040, 3.653265138806914170 ) ) ;
#6116=DIRECTION ( 'NONE',  ( -1.000000000000000000, -7.475397945009582610E-16, 0.000000000000000000 ) ) ;
#6123=CARTESIAN_POINT ( 'NONE',  ( 2.712400463490634017, -4.125000000000058620, -2.714386550172725787 ) ) ;
#6126=CARTESIAN_POINT ( 'NONE',  ( 1.112125432426118499, -1.381875000000161391, 3.661359949639011901 ) ) ;
#6127=CARTESIAN_POINT ( 'NONE',  ( -2.206715255075134774, -5.334838156314726021, 2.588775985198231488 ) ) ;
#6137=ORIENTED_EDGE ( 'NONE', *, *, #5571, .F. ) ;
#6141=CARTESIAN_POINT ( 'NONE',  ( 3.039561480324906473, -2.678749999999966214, -2.029833227700064135 ) ) ;
#6142=EDGE_LOOP ( 'NONE', ( #6365, #1187, #10031, #11778 ) ) ;
#6150=CARTESIAN_POINT ( 'NONE',  ( -3.675091696978340039, 2.375954066961606603, 2.634554458358997042 ) ) ;
#6153=CARTESIAN_POINT ( 'NONE',  ( -1.733190484027876455, 0.04649911033016842360, 4.500000000000000888 ) ) ;
#6157=CARTESIAN_POINT ( 'NONE',  ( -3.069066067673428932, -4.006874999999906706, -1.638984897852511891 ) ) ;
#6168=CARTESIAN_POINT ( 'NONE',  ( 2.743301530724824744, -3.475625000000028386, 2.252549412313605615 ) ) ;
#6171=CARTESIAN_POINT ( 'NONE',  ( 3.104176526174651229, -4.906250000000120792, 2.075311058921220919 ) ) ;
#6179=DIRECTION ( 'NONE',  ( -1.000000000000000000, -2.551930889570659960E-15, 0.000000000000000000 ) ) ;
#6183=DIRECTION ( 'NONE',  ( -1.000000000000000000, 0.000000000000000000, 0.000000000000000000 ) ) ;
#6184=CARTESIAN_POINT ( 'NONE',  ( -0.7999999999999912736, -5.500000000000002665, 0.000000000000000000 ) ) ;
#6185=CARTESIAN_POINT ( 'NONE',  ( -2.972130888462442222, -1.374213562373086450, -2.969983195655016672 ) ) ;
#6188=CARTESIAN_POINT ( 'NONE',  ( -4.296391350416484123, -0.4995676945082700438, -1.627175273956673067E-05 ) ) ;
#6190=FACE_OUTER_BOUND ( 'NONE', #7292, .T. ) ;
#6198=CARTESIAN_POINT ( 'NONE',  ( -3.269128917323805172, -3.406249999999943601, -2.185603562728522853 ) ) ;
#6203=CARTESIAN_POINT ( 'NONE',  ( -3.458861090693667872, -5.280908638085628937, 0.2950975219710819109 ) ) ;
#6204=DIRECTION ( 'NONE',  ( 1.000000000000000000, 2.551930889570660354E-15, 0.000000000000000000 ) ) ;
#6205=CARTESIAN_POINT ( 'NONE',  ( -1.006616814747114065E-29, -2.568816543514387226E-44, 0.000000000000000000 ) ) ;
#6211=ORIENTED_EDGE ( 'NONE', *, *, #194, .T. ) ;
#6213=CARTESIAN_POINT ( 'NONE',  ( -0.6956252696767807331, -3.303750000000123421, 3.503916970779589413 ) ) ;
#6220=CARTESIAN_POINT ( 'NONE',  ( -2.214775092167319492, -5.213036032544459353, -2.777127259766121181 ) ) ;
#6222=CARTESIAN_POINT ( 'NONE',  ( -3.525127887470900223, -0.4995676945082684339, -2.371274685879552369 ) ) ;
#6229=VERTEX_POINT ( 'NONE', #14679 ) ;
#6234=CARTESIAN_POINT ( 'NONE',  ( -0.3703630857574056745, -1.850625000000086340, -3.746264557426716379 ) ) ;
#6238=CARTESIAN_POINT ( 'NONE',  ( -0.7718104722664602679, -3.281249999999995115, -3.872775259196827857 ) ) ;
#6239=LINE ( 'NONE', #307, #14433 ) ;
#6240=FACE_OUTER_BOUND ( 'NONE', #13158, .T. ) ;
#6243=DIRECTION ( 'NONE',  ( -0.8660254037844385966, -2.210036979070412685E-15, 0.5000000000000003331 ) ) ;
#6252=CARTESIAN_POINT ( 'NONE',  ( 0.3227798623957478519, -5.350624999999817888, 3.285751646651179581 ) ) ;
#6255=CARTESIAN_POINT ( 'NONE',  ( 3.740778800480223154, -1.077338562373169495, -1.998207761774829949 ) ) ;
#6269=CARTESIAN_POINT ( 'NONE',  ( -2.938526230868574896, -4.390625000000237144, -2.412868667173103443 ) ) ;
#6270=VERTEX_POINT ( 'NONE', #6188 ) ;
#6272=CARTESIAN_POINT ( 'NONE',  ( 0.001378637340237239689, -4.749213562373086894, 3.755245864738716577 ) ) ;
#6273=CARTESIAN_POINT ( 'NONE',  ( 3.518605591592535387, -1.522500000000036380, 1.455944046807712278 ) ) ;
#6278=CARTESIAN_POINT ( 'NONE',  ( 1.947697749281812607, -5.403728638081555680, 2.678754459976768310 ) ) ;
#6289=CARTESIAN_POINT ( 'NONE',  ( -1.038475776471825984, -3.288125000000012843, 3.420226703972063298 ) ) ;
#6297=CARTESIAN_POINT ( 'NONE',  ( -1.254886650950876925, -0.4995676945082626608, -3.987764699483664188 ) ) ;
#6299=ADVANCED_FACE ( 'NONE', ( #13311 ), #7414, .T. ) ;
#6311=CARTESIAN_POINT ( 'NONE',  ( -0.3615547238505233407, -2.319374999999934239, 3.684823279838126187 ) ) ;
#6312=CARTESIAN_POINT ( 'NONE',  ( -3.613419487966115895, -3.562500000000009326, 1.498272701152596031 ) ) ;
#6316=DIRECTION ( 'NONE',  ( -2.551930889570659960E-15, 1.000000000000000000, 0.000000000000000000 ) ) ;
#6329=CARTESIAN_POINT ( 'NONE',  ( -3.191126515704096001, -6.069374228118336490, -0.3131016245760978034 ) ) ;
#6333=CARTESIAN_POINT ( 'NONE',  ( -0.9755776780686565841, -4.881874999999863185, -3.218989981404408951 ) ) ;
#6345=EDGE_CURVE ( 'NONE', #8406, #11643, #13272, .T. ) ;
#6350=CARTESIAN_POINT ( 'NONE',  ( 3.506874188274308413, -3.078124999999926281, -1.873277435140577429 ) ) ;
#6361=CARTESIAN_POINT ( 'NONE',  ( -0.8000000000000178080, 9.500000000000000000, 0.000000000000000000 ) ) ;
#6365=ORIENTED_EDGE ( 'NONE', *, *, #4996, .T. ) ;
#6366=CARTESIAN_POINT ( 'NONE',  ( 3.341236413112297576, -1.663124999999897824, -1.787503410618120236 ) ) ;
#6370=AXIS2_PLACEMENT_3D ( 'NONE', #9692, #9854, #12269 ) ;
#6372=CARTESIAN_POINT ( 'NONE',  ( 3.897114317029974018, 9.945166405816858860E-15, -2.250000000000001332 ) ) ;
#6374=CARTESIAN_POINT ( 'NONE',  ( -3.979857382319186510, -0.4995676945082694886, -1.548798448790204452 ) ) ;
#6387=CARTESIAN_POINT ( 'NONE',  ( 0.3615547238501363725, -2.350625000000046150, 3.680709139401309837 ) ) ;
#6388=CARTESIAN_POINT ( 'NONE',  ( -1.780457766239074071E-14, 9.500000000000000000, 6.182228413854880884E-29 ) ) ;
#6390=CARTESIAN_POINT ( 'NONE',  ( -3.630950894689927821, -4.453124999999883649, -1.099983568547476143 ) ) ;
#6405=CARTESIAN_POINT ( 'NONE',  ( 2.325173090398219067, -5.459999999999847198, 2.323431042901937360 ) ) ;
#6409=CARTESIAN_POINT ( 'NONE',  ( 2.325173090398219067, -5.459999999999847198, 2.323431042901936916 ) ) ;
#6422=CARTESIAN_POINT ( 'NONE',  ( 4.096389842826703820, -2.015625000000050182, -0.4049582849837481402 ) ) ;
#6425=CONICAL_SURFACE ( 'NONE', #13105, 3.637955631634646192, 0.1308996938995775905 ) ;
#6433=DIRECTION ( 'NONE',  ( 1.000000000000000000, 8.284258017326334836E-16, 0.000000000000000000 ) ) ;
#6436=CONICAL_SURFACE ( 'NONE', #12127, 4.500000000000000888, 1.396263401595466691 ) ;
#6438=ORIENTED_EDGE ( 'NONE', *, *, #14711, .F. ) ;
#6441=DIRECTION ( 'NONE',  ( -9.422394424380274864E-16, 1.000000000000000000, -0.000000000000000000 ) ) ;
#6442=CARTESIAN_POINT ( 'NONE',  ( -1.418005212499603429, -2.272500000000021281, 3.426931839692804793 ) ) ;
#6446=CARTESIAN_POINT ( 'NONE',  ( 1.233021357193251788, -0.4995676945082553888, -3.929992886820973474 ) ) ;
#6448=FACE_OUTER_BOUND ( 'NONE', #4113, .T. ) ;
#6459=CARTESIAN_POINT ( 'NONE',  ( 3.518605591592535387, -1.522500000000036380, 1.455944046807712278 ) ) ;
#6461=CARTESIAN_POINT ( 'NONE',  ( 2.130457310823663519, -4.156249999999911182, -3.186652721750134809 ) ) ;
#6465=CARTESIAN_POINT ( 'NONE',  ( 1.227202584385329587, -1.203124999999989342, -4.041673972266214498 ) ) ;
#6470=DIRECTION ( 'NONE',  ( 1.000000000000000000, 0.000000000000000000, -6.982962677686266711E-15 ) ) ;
#6471=VERTEX_POINT ( 'NONE', #14898 ) ;
#6483=CARTESIAN_POINT ( 'NONE',  ( 2.393563981450126388, -4.710000000000058584, -2.395350030107596506 ) ) ;
#6484=ORIENTED_EDGE ( 'NONE', *, *, #14162, .F. ) ;
#6490=CARTESIAN_POINT ( 'NONE',  ( -4.030856054181176873, -2.515624999999848121, 0.3959303163381804880 ) ) ;
#6497=DIRECTION ( 'NONE',  ( -2.551930889570659960E-15, 1.000000000000000000, 0.000000000000000000 ) ) ;
#6509=CARTESIAN_POINT ( 'NONE',  ( -3.795858268372354960, -1.053749999999936460, -0.7536008350790910360 ) ) ;
#6534=B_SPLINE_CURVE_WITH_KNOTS ( 'NONE', 3,
 ( #2282, #9265, #11672, #14230, #4625, #1041 ),
 .UNSPECIFIED., .F., .F.,
 ( 4, 2, 4 ),
 ( 0.000000000000000000, 0.001172976575130644768, 0.002345953150261289536 ),
 .UNSPECIFIED. ) ;
#6537=CARTESIAN_POINT ( 'NONE',  ( 3.553279128418493915, -4.062500000000332179, -1.470728592776388455 ) ) ;
#6541=CARTESIAN_POINT ( 'NONE',  ( 0.001544386136394801726, -0.7500000000000344169, 4.283781196144704317 ) ) ;
#6544=AXIS2_PLACEMENT_3D ( 'NONE', #5838, #4667, #7457 ) ;
#6546=ORIENTED_EDGE ( 'NONE', *, *, #10366, .T. ) ;
#6555=CARTESIAN_POINT ( 'NONE',  ( -2.763334307196396722, -5.178749999999838316, 1.847896475581856324 ) ) ;
#6558=FACE_OUTER_BOUND ( 'NONE', #9458, .T. ) ;
#6569=ORIENTED_EDGE ( 'NONE', *, *, #15102, .F. ) ;
#6570=CARTESIAN_POINT ( 'NONE',  ( 3.434081308463064364, -1.906250000000116795, 2.295896066549416581 ) ) ;
#6571=VERTEX_POINT ( 'NONE', #8394 ) ;
#6588=CARTESIAN_POINT ( 'NONE',  ( -2.355664480073799805, -2.225624999999979092, 2.872538697791624962 ) ) ;
#6597=CARTESIAN_POINT ( 'NONE',  ( 3.542101689960518662, -0.4995676945082338505, 1.737881650567584924 ) ) ;
#6609=STYLED_ITEM ( 'NONE', ( #7424 ), #442 ) ;
#6611=B_SPLINE_CURVE_WITH_KNOTS ( 'NONE', 3,
 ( #11332, #7473, #4047, #3032, #549, #12507, #10081, #10010, #14586, #12190, #3966, #699 ),
 .UNSPECIFIED., .F., .F.,
 ( 4, 2, 2, 2, 2, 4 ),
 ( 2.544323688695237330E-07, 0.001342108318545689885, 0.002013035261634099626, 0.002683962204722509584, 0.004025816090899331234, 0.005367669977076151150 ),
 .UNSPECIFIED. ) ;
#6616=AXIS2_PLACEMENT_3D ( 'NONE', #10599, #9428, #14244 ) ;
#6617=CARTESIAN_POINT ( 'NONE',  ( 2.507317702870323739, -0.4443749999999629940, 3.052905756198839970 ) ) ;
#6620=CARTESIAN_POINT ( 'NONE',  ( 3.796719365261179480, -2.062499999999996003, -1.574265350336458313 ) ) ;
#6626=CARTESIAN_POINT ( 'NONE',  ( 3.016622086615760256, -0.8749999999999454880, 3.018230387793254810 ) ) ;
#6630=CARTESIAN_POINT ( 'NONE',  ( -5.196152422706630247, 0.1227504548087275521, -7.569115911492098221E-16 ) ) ;
#6635=CIRCLE ( 'NONE', #1159, 2.320576762250993852 ) ;
#6636=CARTESIAN_POINT ( 'NONE',  ( 1.553520276525307997, -5.413125000000014175, 2.903814772855817239 ) ) ;
#6637=EDGE_CURVE ( 'NONE', #8592, #4923, #13783, .T. ) ;
#6643=CARTESIAN_POINT ( 'NONE',  ( -3.099447957106487461, -0.4995676945082667686, 2.829882024851861466 ) ) ;
#6645=DIRECTION ( 'NONE',  ( 0.000000000000000000, -0.000000000000000000, -1.000000000000000000 ) ) ;
#6649=ORIENTED_EDGE ( 'NONE', *, *, #346, .T. ) ;
#6653=CARTESIAN_POINT ( 'NONE',  ( -3.582436959730881831, -2.421875000000131450, -1.916069189016956331 ) ) ;
#6654=ORIENTED_EDGE ( 'NONE', *, *, #8010, .F. ) ;
#6666=CARTESIAN_POINT ( 'NONE',  ( 0.3615547238501363170, -2.350625000000046150, 3.680709139401400432 ) ) ;
#6671=DIRECTION ( 'NONE',  ( -2.551930889570658776E-15, 1.000000000000000000, 0.000000000000000000 ) ) ;
#6676=VERTEX_POINT ( 'NONE', #3816 ) ;
#6678=EDGE_CURVE ( 'NONE', #6676, #12263, #11973, .T. ) ;
#6685=CARTESIAN_POINT ( 'NONE',  ( -3.459955264279602094, -6.467963562372781361, -0.6891510056894314395 ) ) ;
#6686=CARTESIAN_POINT ( 'NONE',  ( 2.697785604507370483, -1.459999999999946008, 2.699193867783821865 ) ) ;
#6687=CARTESIAN_POINT ( 'NONE',  ( 1.186295216973591859, -2.203125000000055067, -3.915803815994934656 ) ) ;
#6692=CARTESIAN_POINT ( 'NONE',  ( -2.727692609523614475, -0.6406250000000671685, 3.321895092029963248 ) ) ;
#6698=ADVANCED_FACE ( 'NONE', ( #3965 ), #8693, .F. ) ;
#6699=ORIENTED_EDGE ( 'NONE', *, *, #11897, .T. ) ;
#6701=EDGE_LOOP ( 'NONE', ( #7140, #9743, #1734 ) ) ;
#6706=CARTESIAN_POINT ( 'NONE',  ( 2.417253850352953481, -4.460000000000003517, 2.418486108946755309 ) ) ;
#6714=CARTESIAN_POINT ( 'NONE',  ( 2.991299100910195019, -4.663125000000096776, -1.600316903339956243 ) ) ;
#6717=EDGE_CURVE ( 'NONE', #7102, #12263, #13052, .T. ) ;
#6719=EDGE_LOOP ( 'NONE', ( #15030, #5223, #10866, #15046 ) ) ;
#6720=CARTESIAN_POINT ( 'NONE',  ( -4.125408418587476866, -0.5468750000000269784, 1.250226324283678192 ) ) ;
#6722=CARTESIAN_POINT ( 'NONE',  ( 2.518194796243166333, -3.139838562372984310, -3.066784450280832797 ) ) ;
#6734=CARTESIAN_POINT ( 'NONE',  ( -3.080079348812820861, -0.1943750000000852018, 2.526399673485165032 ) ) ;
#6735=ORIENTED_EDGE ( 'NONE', *, *, #10376, .F. ) ;
#6736=CARTESIAN_POINT ( 'NONE',  ( -3.579091221414520518, -2.038125000000108322, -1.084269867492441586 ) ) ;
#6740=CARTESIAN_POINT ( 'NONE',  ( 3.992217303742939816, -0.4995676945082484499, -0.08329250675602982434 ) ) ;
#6742=EDGE_CURVE ( 'NONE', #1927, #14968, #4637, .T. ) ;
#6749=ORIENTED_EDGE ( 'NONE', *, *, #518, .T. ) ;
#6753=CARTESIAN_POINT ( 'NONE',  ( -2.574205329084022331, -5.624213562373249431, 2.572875433237910681 ) ) ;
#6755=CARTESIAN_POINT ( 'NONE',  ( -3.693744850241972077, -1.131875000000025722, 1.119430425315776523 ) ) ;
#6757=CARTESIAN_POINT ( 'NONE',  ( -2.852666340614860463, -2.624999999999946265, 2.854740429567705018 ) ) ;
#6762=CARTESIAN_POINT ( 'NONE',  ( 3.331139167509270749, 2.239389106484354297, 3.230297714791237507 ) ) ;
#6763=CARTESIAN_POINT ( 'NONE',  ( 3.935370341889717682, -0.9375000000000351941, 1.628420556316443557 ) ) ;
#6776=CARTESIAN_POINT ( 'NONE',  ( -3.468991550463924156, -4.085000000000062137, -0.0008868951686453910126 ) ) ;
#6787=ORIENTED_EDGE ( 'NONE', *, *, #9420, .F. ) ;
#6796=CARTESIAN_POINT ( 'NONE',  ( -2.948053448091068507, -1.625000000000079936, 2.946489148067756858 ) ) ;
#6798=CARTESIAN_POINT ( 'NONE',  ( -3.971205795094620683, -2.530463562372954112, 0.7888322869661125170 ) ) ;
#6812=CARTESIAN_POINT ( 'NONE',  ( 3.291891004236185747, -4.921874999999971578, 1.757997479805845975 ) ) ;
#6816=CARTESIAN_POINT ( 'NONE',  ( 0.7342756466162075890, -1.803750000000060361, -3.698544502508174681 ) ) ;
#6820=CARTESIAN_POINT ( 'NONE',  ( 3.931003132613788420, -0.4995676945082495601, 0.5405018855187671001 ) ) ;
#6821=CARTESIAN_POINT ( 'NONE',  ( 3.530157234965975555, -5.226201182446649440, -2.246195850846843811E-13 ) ) ;
#6828=ORIENTED_EDGE ( 'NONE', *, *, #125, .F. ) ;
#6829=CARTESIAN_POINT ( 'NONE',  ( -3.069066067673342779, -4.006874999999906706, -1.638984897852512113 ) ) ;
#6833=CARTESIAN_POINT ( 'NONE',  ( -3.050941831956043515, -5.405463562373032715, -2.036948827022558195 ) ) ;
#6835=CARTESIAN_POINT ( 'NONE',  ( -3.080079348812917228, -0.1943750000000852018, 2.526399673485165032 ) ) ;
#6836=CARTESIAN_POINT ( 'NONE',  ( 0.7355390728087518593, -5.399066645772633066, 3.225404868253181956 ) ) ;
#6838=CARTESIAN_POINT ( 'NONE',  ( 3.434081308463064364, -1.906250000000116795, 2.295896066549416581 ) ) ;
#6857=CARTESIAN_POINT ( 'NONE',  ( 0.4577183132938494881, 2.374744442185180215, -4.499999999999999112 ) ) ;
#6868=VECTOR ( 'NONE', #13004, 1000.000000000000114 ) ;
#6871=CARTESIAN_POINT ( 'NONE',  ( -0.8118119174735605181, -1.718749999999964917, 4.075604227461077755 ) ) ;
#6873=CARTESIAN_POINT ( 'NONE',  ( 2.540175370683049216, -2.858588562373145070, 3.096875823539658068 ) ) ;
#6882=FACE_OUTER_BOUND ( 'NONE', #2936, .T. ) ;
#6883=DIRECTION ( 'NONE',  ( -1.000000000000000000, -1.747085166004344019E-15, 0.000000000000000000 ) ) ;
#6887=CARTESIAN_POINT ( 'NONE',  ( -3.385327830538905847, -5.437500000000312639, -1.400787550305463203 ) ) ;
#6892=CARTESIAN_POINT ( 'NONE',  ( 0.3615547238501363725, -2.350625000000046150, 3.680709139401309837 ) ) ;
#6906=CARTESIAN_POINT ( 'NONE',  ( -1.287538504857992594, -4.897500000000167830, -3.105113058795574865 ) ) ;
#6909=ORIENTED_EDGE ( 'NONE', *, *, #2013, .T. ) ;
#6910=CARTESIAN_POINT ( 'NONE',  ( -3.116388545455692771, -6.421088562373019393, -1.666773181135335902 ) ) ;
#6911=CARTESIAN_POINT ( 'NONE',  ( -2.746234728672232173, -0.9599999999999920819, -2.744228674164098436 ) ) ;
#6913=CARTESIAN_POINT ( 'NONE',  ( 1.869272562217232592, -3.171875000000011990, -3.494952631674145938 ) ) ;
#6929=CARTESIAN_POINT ( 'NONE',  ( 2.192040893887766018, 1.873195365157829473, -4.499999999999998224 ) ) ;
#6937=ADVANCED_FACE ( 'NONE', ( #10382, #2165 ), #9375, .F. ) ;
#6938=ORIENTED_EDGE ( 'NONE', *, *, #3195, .F. ) ;
#6942=CARTESIAN_POINT ( 'NONE',  ( -4.166404709851690313, -1.484374999999892752, -0.4114723880711238513 ) ) ;
#6944=CARTESIAN_POINT ( 'NONE',  ( 1.188938652636758464, -2.202338562373083342, -3.915676949994142397 ) ) ;
#6947=CARTESIAN_POINT ( 'NONE',  ( 4.353714886931038031, 2.288586792248405555, -1.459144614166440146 ) ) ;
#6956=CARTESIAN_POINT ( 'NONE',  ( 1.071213019063891991, -5.203124999999990230, -3.535999920922690443 ) ) ;
#6958=CARTESIAN_POINT ( 'NONE',  ( -3.657957510581538507, -2.116249999999859632, 0.7266254446581354998 ) ) ;
#6973=CARTESIAN_POINT ( 'NONE',  ( -2.874539946219752728, -4.178749999999989306, 1.919644203647528524 ) ) ;
#6978=CARTESIAN_POINT ( 'NONE',  ( 2.866736077644334912, -5.108588562372962549, -2.351425311670667817 ) ) ;
#6989=CARTESIAN_POINT ( 'NONE',  ( -3.199287326323787095, -5.038124999999881837, -0.9691876696830878934 ) ) ;
#7001=CARTESIAN_POINT ( 'NONE',  ( -0.3378546177656944205, -4.319374999999974207, 3.421346328963575711 ) ) ;
#7002=VECTOR ( 'NONE', #3584, 1000.000000000000000 ) ;
#7015=ORIENTED_EDGE ( 'NONE', *, *, #10238, .F. ) ;
#7018=CARTESIAN_POINT ( 'NONE',  ( -3.428831060970971567, 0.3906249999999135136, 2.812429823455744327 ) ) ;
#7021=CARTESIAN_POINT ( 'NONE',  ( 1.891342852395442531, -2.827338562373011399, 3.535359886477475566 ) ) ;
#7025=AXIS2_PLACEMENT_3D ( 'NONE', #6095, #9324, #3591 ) ;
#7037=CARTESIAN_POINT ( 'NONE',  ( 2.481497852716000097, -0.7256250000000298295, -3.025965195089417747 ) ) ;
#7040=CARTESIAN_POINT ( 'NONE',  ( 2.674095735623811088, -1.709999999999972209, -2.676057788957662886 ) ) ;
#7043=EDGE_CURVE ( 'NONE', #13047, #5763, #646, .T. ) ;
#7051=EDGE_LOOP ( 'NONE', ( #2077, #8305, #7481, #6938, #6828 ) ) ;
#7058=CARTESIAN_POINT ( 'NONE',  ( -1.914696782014857712, -4.241249999999832987, 2.867854448260448219 ) ) ;
#7063=CARTESIAN_POINT ( 'NONE',  ( -3.491779696971169411, -4.561713562373101993, 1.447843152864476624 ) ) ;
#7069=CARTESIAN_POINT ( 'NONE',  ( -5.196152422706634688, 1.678847577293359539, -8.911270275552416508E-16 ) ) ;
#7073=CARTESIAN_POINT ( 'NONE',  ( 0.3421672931281763419, -3.819374999999898268, -3.487344533451358863 ) ) ;
#7085=CARTESIAN_POINT ( 'NONE',  ( 3.520079602834293109, -3.569375000000153619, 0.3476102605345692265 ) ) ;
#7089=CARTESIAN_POINT ( 'NONE',  ( 0.7330380326264336333, -4.781250000000259348, 3.678172007241774732 ) ) ;
#7092=CARTESIAN_POINT ( 'NONE',  ( -4.296391350416484123, -0.4995676945082700438, -1.627175273956673067E-05 ) ) ;
#7095=B_SPLINE_CURVE_WITH_KNOTS ( 'NONE', 3,
 ( #7946, #8889, #13627, #12460 ),
 .UNSPECIFIED., .F., .F.,
 ( 4, 4 ),
 ( 0.006950528372497996078, 0.009557525114560322041 ),
 .UNSPECIFIED. ) ;
#7101=ORIENTED_EDGE ( 'NONE', *, *, #14908, .F. ) ;
#7102=VERTEX_POINT ( 'NONE', #5987 ) ;
#7106=CARTESIAN_POINT ( 'NONE',  ( -1.246598846679689343, -0.7023385623730667993, 4.105542770413508791 ) ) ;
#7120=CARTESIAN_POINT ( 'NONE',  ( -0.3668491701747607636, -4.734375000000160760, 3.738752075031570588 ) ) ;
#7123=CARTESIAN_POINT ( 'NONE',  ( -1.834300037444539511, -0.9131249999999379030, -3.428720741157346374 ) ) ;
#7124=CARTESIAN_POINT ( 'NONE',  ( 1.682902201845278611, -5.420849775684215999, 2.811263474311217259 ) ) ;
#7135=ADVANCED_FACE ( 'NONE', ( #14848 ), #10535, .F. ) ;
#7138=CARTESIAN_POINT ( 'NONE',  ( 1.394838545734257140, -2.772499999999996856, -3.364978284447635026 ) ) ;
#7140=ORIENTED_EDGE ( 'NONE', *, *, #3195, .T. ) ;
#7142=CARTESIAN_POINT ( 'NONE',  ( -2.092043339069166841, -4.655463562372927022, 3.133452599004876493 ) ) ;
#7151=CARTESIAN_POINT ( 'NONE',  ( -2.773226354234704427, -3.194375000000006182, 2.274732928208734961 ) ) ;
#7160=CARTESIAN_POINT ( 'NONE',  ( 1.656526992905777318, -3.756875000000012399, -3.097233728230734062 ) ) ;
#7162=CARTESIAN_POINT ( 'NONE',  ( 3.897114317029974462, 9.945166405816860437E-15, 2.249999999999999556 ) ) ;
#7172=CONICAL_SURFACE ( 'NONE', #3936, 4.500000000000000888, 1.396263401595466691 ) ;
#7181=CARTESIAN_POINT ( 'NONE',  ( 4.363871257596563247, 0.01562500000001383962, 0.4309836735954339360 ) ) ;
#7183=CARTESIAN_POINT ( 'NONE',  ( -2.023153048893557848, -0.6710885623731100980, 3.788336601472766407 ) ) ;
#7192=CARTESIAN_POINT ( 'NONE',  ( -1.673688575075003955E-15, 4.650702586819541295, 0.000000000000000000 ) ) ;
#7196=CARTESIAN_POINT ( 'NONE',  ( 2.153747138339810796, -3.843749999999965361, 3.220761568642789729 ) ) ;
#7198=CARTESIAN_POINT ( 'NONE',  ( -2.135074830120813782, -1.241249999999904707, 3.197897516496418291 ) ) ;
#7200=CARTESIAN_POINT ( 'NONE',  ( -1.442844940792075370, -5.353007078811534036, 3.043495819154527382 ) ) ;
#7208=ORIENTED_EDGE ( 'NONE', *, *, #12659, .T. ) ;
#7210=CARTESIAN_POINT ( 'NONE',  ( 3.520079602834293553, -3.569375000000153619, 0.3476102605345473551 ) ) ;
#7221=CARTESIAN_POINT ( 'NONE',  ( 3.273328345814555007, -3.522500000000126974, 1.356842221127619874 ) ) ;
#7231=B_SPLINE_SURFACE_WITH_KNOTS ( 'NONE', 1, 3, ( 
 ( #8055, #12498, #6685, #4261, #6910, #11394, #12794, #9138, #4488, #11475, #11323, #691, #841, #12574, #10375, #15100, #5517, #2161, #1935, #7907, #12638, #4194, #613, #5367, #3244, #10075, #10219, #8916, #13733, #14952, #9070, #3024, #13655, #3102, #4345, #13809, #5596, #2003, #6753, #10303, #15031, #13875, #7768, #1857, #5443, #7976, #2083, #6833, #920, #10140, #14032, #10530, #14108, #351, #9811, #12874, #10611, #14541, #1515, #5097, #6978, #14179, #992, #2234, #11782, #9292, #5746, #264, #7427, #11702, #10448, #2312, #4568, #13322, #10984, #6272, #1068, #1227, #15333, #7142, #3923, #4654, #2394, #7063, #5015, #15258, #8648, #2682, #11631, #12146, #13393, #2749, #9370, #1153, #11861, #3404, #5985, #3556, #8140, #5911, #5826, #15179, #3478, #8576, #8212, #8290, #14467, #13033, #12951, #4726, #9730, #9441, #10687, #3850, #12534, #9959, #4161, #8885, #13623, #12310, #2990, #3993, #11364, #14915, #8724, #12456, #731, #7505, #5483, #1597, #10181, #11067, #13993, #9104, #3213, #3368, #10342, #8177, #12907, #13916, #10577, #15068, #10411, #15140, #6722, #11748, #3144, #5787, #11437, #13845, #8101, #1032, #4613, #12677, #15301, #2051, #6873, #7021, #11517, #4384, #4693, #958, #2126, #11662, #12838, #9256, #9405, #9336, #1115, #7943, #6798, #4533, #803, #2273, #5875, #8020, #9174, #7877, #12758, #12610, #1972, #14991, #880, #5643, #6944, #11594, #10495, #5712, #3289, #2201, #4457, #15223, #14075, #3444, #5560, #10262, #2353, #10733, #182, #8557, #6106, #13083, #97, #2667, #8411, #4848, #12134, #2502, #3602, #2436, #8251, #13306, #9710, #10650, #9559, #14303, #251, #1429, #3680, #6185, #9481, #4928, #21, #10966, #11901, #10817, #9637, #4766, #3833, #14371, #13151, #1503, #6255, #12996, #14221, #328, #3749, #5077, #14142, #3517, #10894, #7252, #14446, #11978, #1346, #4997, #8339, #8479, #7106, #7183, #13223, #11828, #2583, #7332, #1193, #12060, #5952, #1262 ),
 ( #6027, #11188, #12436, #10024, #7487, #2819, #7711, #11120, #4144, #7644, #1799, #3978, #12368, #13456, #1659, #8707, #13536, #12519, #3046, #8632, #14756, #7569, #8866, #2974, #1881, #12205, #12287, #6409, #13676, #6636, #11044, #2900, #11347, #14826, #714, #5160, #13606, #14523, #417, #6555, #1580, #3908, #11273, #5393, #9869, #13380, #492, #2736, #637, #8936, #4212, #9790, #6333, #13895, #939, #14054, #13830, #5696, #11497, #3345, #4364, #4589, #1012, #5461, #5766, #3424, #8158, #3199, #15051, #10394, #6706, #15120, #7996, #11414, #4439, #781, #7001, #11727, #2181, #2253, #12736, #8078, #2105, #3124, #7927, #12815, #6776, #4512, #3266, #14894, #14973, #9234, #9088, #2028, #10241, #13753, #9388, #13203, #8537, #12975, #7160, #3, #7393, #1243, #13285, #14351, #4977, #11954, #7085, #1171, #1321, #8315, #6168, #231, #6003, #2647, #13058, #13131, #6085, #4675, #9688, #1093, #3728, #14124, #11806, #10797, #7312, #12040, #5849, #2413, #10553, #9461, #10710, #9538, #3497, #3809, #14200, #75, #4828, #162, #1410, #14282, #8233, #2335, #5930, #10630, #3580, #2954, #2719, #14806, #5288, #9922, #12182, #14502, #1555, #474, #8688, #12417, #5210, #5369, #6387, #6311, #8918, #11020, #14655, #614, #5139, #13363, #13656, #4038, #8767, #10000, #7623, #2878, #3026, #1781, #12117, #7464, #394, #13510, #304, #6234, #10943, #1636, #2794, #5054, #12345, #9767, #3889, #9850, #3962, #7548, #14730, #1708, #4121, #6459, #12265, #11169, #6686, #11395, #13951, #760, #2004, #11324, #692, #4346, #9139, #2162, #15032, #5518, #9071, #11632, #6755, #13811, #5747, #11476, #12575, #10220, #1859, #6911, #3325, #4263, #3178, #12639, #9212, #10377, #842, #15101, #3104, #13876, #8991, #4569, #14953, #4420, #3245, #13734, #12796, #7978, #5598, #10450, #994, #6617, #1936, #15180, #12714, #14034, #7769, #12499, #4489, #10305, #8056, #2084, #6835, #5444, #11557, #921, #10141, #5681 ) ),
 .UNSPECIFIED., .F., .F., .F.,
 ( 2, 2 ),
 ( 4, 2, 2, 2, 2, 2, 2, 2, 2, 2, 2, 2, 2, 2, 2, 2, 2, 2, 2, 2, 2, 2, 2, 2, 2, 2, 2, 2, 2, 2, 2, 2, 2, 2, 2, 2, 2, 2, 2, 2, 2, 2, 2, 2, 2, 2, 2, 2, 2, 2, 2, 2, 2, 2, 2, 2, 2, 2, 2, 2, 2, 2, 2, 2, 2, 2, 2, 2, 2, 2, 2, 2, 2, 2, 2, 2, 2, 2, 2, 2, 2, 2, 2, 2, 2, 2, 2, 2, 2, 2, 2, 2, 2, 2, 2, 2, 2, 2, 2, 2, 2, 2, 2, 2, 2, 2, 2, 2, 2, 2, 2, 2, 2, 2, 2, 2, 2, 2, 2, 2, 2, 2, 2, 2, 2, 2, 2, 2, 4 ),
 ( 0.000000000000000000, 1.000000000000000000 ),
 ( 0.000000000000000000, 0.007812500000000000000, 0.01562500000000000000, 0.02343750000000000000, 0.03125000000000000000, 0.03906250000000000000, 0.04687500000000000000, 0.05468750000000000000, 0.06250000000000000000, 0.07031250000000000000, 0.07812500000000000000, 0.08593750000000000000, 0.09375000000000000000, 0.1015625000000000000, 0.1093750000000000000, 0.1171875000000000000, 0.1250000000000000000, 0.1328125000000000000, 0.1406250000000000000, 0.1484375000000000000, 0.1562500000000000000, 0.1640625000000000000, 0.1718750000000000000, 0.1796875000000000000, 0.1875000000000000000, 0.1953125000000000000, 0.2031250000000000000, 0.2109375000000000000, 0.2187500000000000000, 0.2265625000000000000, 0.2343750000000000000, 0.2421875000000000000, 0.2500000000000000000, 0.2578125000000000000, 0.2656250000000000000, 0.2734375000000000000, 0.2812500000000000000, 0.2890625000000000000, 0.2968750000000000000, 0.3046875000000000000, 0.3125000000000000000, 0.3203125000000000000, 0.3281250000000000000, 0.3359375000000000000, 0.3437500000000000000, 0.3515625000000000000, 0.3593750000000000000, 0.3671875000000000000, 0.3750000000000000000, 0.3828125000000000000, 0.3906250000000000000, 0.3984375000000000000, 0.4062500000000000000, 0.4140625000000000000, 0.4218750000000000000, 0.4296875000000000000, 0.4375000000000000000, 0.4453125000000000000, 0.4531250000000000000, 0.4609375000000000000, 0.4687500000000000000, 0.4765625000000000000, 0.4843750000000000000, 0.4921875000000000000, 0.5000000000000000000, 0.5078125000000000000, 0.5156250000000000000, 0.5234375000000000000, 0.5312500000000000000, 0.5390625000000000000, 0.5468750000000000000, 0.5546875000000000000, 0.5625000000000000000, 0.5703125000000000000, 0.5781250000000000000, 0.5859375000000000000, 0.5937500000000000000, 0.6015625000000000000, 0.6093750000000000000, 0.6171875000000000000, 0.6250000000000000000, 0.6328125000000000000, 0.6406250000000000000, 0.6484375000000000000, 0.6562500000000000000, 0.6640625000000000000, 0.6718750000000000000, 0.6796875000000000000, 0.6875000000000000000, 0.6953125000000000000, 0.7031250000000000000, 0.7109375000000000000, 0.7187500000000000000, 0.7265625000000000000, 0.7343750000000000000, 0.7421875000000000000, 0.7500000000000000000, 0.7578125000000000000, 0.7656250000000000000, 0.7734375000000000000, 0.7812500000000000000, 0.7890625000000000000, 0.7968750000000000000, 0.8046875000000000000, 0.8125000000000000000, 0.8203125000000000000, 0.8281250000000000000, 0.8359375000000000000, 0.8437500000000000000, 0.8515625000000000000, 0.8593750000000000000, 0.8671875000000000000, 0.8750000000000000000, 0.8828125000000000000, 0.8906250000000000000, 0.8984375000000000000, 0.9062500000000000000, 0.9140625000000000000, 0.9218750000000000000, 0.9296875000000000000, 0.9375000000000000000, 0.9453125000000000000, 0.9531250000000000000, 0.9609375000000000000, 0.9687500000000000000, 0.9765625000000000000, 0.9843750000000000000, 0.9921875000000000000, 1.000000000000000000 ),
 .UNSPECIFIED. ) ;
#7234=FACE_OUTER_BOUND ( 'NONE', #1064, .T. ) ;
#7247=VERTEX_POINT ( 'NONE', #6372 ) ;
#7248=DIRECTION ( 'NONE',  ( -2.551930889570660354E-15, 1.000000000000000000, 0.000000000000000000 ) ) ;
#7249=AXIS2_PLACEMENT_3D ( 'NONE', #15053, #7931, #11646 ) ;
#7251=EDGE_CURVE ( 'NONE', #11935, #7479, #11940, .T. ) ;
#7252=CARTESIAN_POINT ( 'NONE',  ( 2.709998298289202356, -0.8585885623730556970, 3.299714903563142787 ) ) ;
#7255=AXIS2_PLACEMENT_3D ( 'NONE', #12686, #13005, #9266 ) ;
#7258=CARTESIAN_POINT ( 'NONE',  ( 4.463089466550662188, 2.239389106484356518, -1.269702285208761605 ) ) ;
#7270=CARTESIAN_POINT ( 'NONE',  ( -3.771471614353887336, -4.484375000000117240, -0.3724498170710106582 ) ) ;
#7271=ORIENTED_EDGE ( 'NONE', *, *, #6742, .T. ) ;
#7282=CARTESIAN_POINT ( 'NONE',  ( 2.811606400754406820, -5.337890745103998746, 1.889891293729461186 ) ) ;
#7290=CARTESIAN_POINT ( 'NONE',  ( -3.581969766213484618, -3.100624999999847198, 0.3518610084922548231 ) ) ;
#7292=EDGE_LOOP ( 'NONE', ( #13807, #6105, #5996, #4843 ) ) ;
#7298=CARTESIAN_POINT ( 'NONE',  ( -0.8000000000000114797, 9.500000000000000000, 0.000000000000000000 ) ) ;
#7301=TOROIDAL_SURFACE ( 'NONE', #13245, 2.931404194366992400, 0.5000000000000000000 ) ;
#7302=CARTESIAN_POINT ( 'NONE',  ( -3.468991550463924156, -4.085000000000062137, -0.0008868951686453910126 ) ) ;
#7304=ORIENTED_EDGE ( 'NONE', *, *, #8372, .T. ) ;
#7312=CARTESIAN_POINT ( 'NONE',  ( -3.319861881881159160, -3.147500000000079456, 1.374129751973758307 ) ) ;
#7314=CARTESIAN_POINT ( 'NONE',  ( -1.438726384651785040, -4.687499999999733546, 3.477001582427886817 ) ) ;
#7315=CARTESIAN_POINT ( 'NONE',  ( -9.797174393178927223E-17, 9.500000000000000000, 0.000000000000000000 ) ) ;
#7329=DIRECTION ( 'NONE',  ( 1.000000000000000000, 2.551930889570660354E-15, 0.000000000000000000 ) ) ;
#7331=CARTESIAN_POINT ( 'NONE',  ( -0.8607816759752345837, 0.2812500000001324496, 4.335577264497109340 ) ) ;
#7332=CARTESIAN_POINT ( 'NONE',  ( -3.797812870634804217, -0.5773385623730058480, 2.031732732842940425 ) ) ;
#7349=CARTESIAN_POINT ( 'NONE',  ( -3.898923295066525352, -3.515625000000077716, 0.3854469994812330658 ) ) ;
#7350=EDGE_LOOP ( 'NONE', ( #9555, #8309, #14596 ) ) ;
#7352=CARTESIAN_POINT ( 'NONE',  ( -3.795858268372354516, -1.053749999999936460, -0.7536008350790791566 ) ) ;
#7367=ADVANCED_FACE ( 'NONE', ( #5661 ), #914, .F. ) ;
#7370=CARTESIAN_POINT ( 'NONE',  ( -2.773226354234704427, -3.194375000000006182, 2.274732928208646587 ) ) ;
#7375=AXIS2_PLACEMENT_3D ( 'NONE', #3732, #10947, #8463 ) ;
#7393=CARTESIAN_POINT ( 'NONE',  ( 2.488663048653545928, -3.709999999999854303, -2.487386788893799494 ) ) ;
#7396=CARTESIAN_POINT ( 'NONE',  ( -2.390027884620886667, -4.640624999999809042, 2.914437415443186907 ) ) ;
#7404=ORIENTED_EDGE ( 'NONE', *, *, #8500, .F. ) ;
#7409=CARTESIAN_POINT ( 'NONE',  ( -3.322613055092911605, -5.069375000000116316, -0.3280989749989033366 ) ) ;
#7411=B_SPLINE_CURVE_WITH_KNOTS ( 'NONE', 3,
 ( #8748, #13494, #1306, #9599 ),
 .UNSPECIFIED., .F., .F.,
 ( 4, 4 ),
 ( 2.309401076760371583E-07, 0.002598307151460989804 ),
 .UNSPECIFIED. ) ;
#7414=SPHERICAL_SURFACE ( 'NONE', #15257, 0.8600000000000014300 ) ;
#7424=PRESENTATION_STYLE_ASSIGNMENT (( #5091 ) ) ;
#7425=CARTESIAN_POINT ( 'NONE',  ( 1.111882196364886832, -4.203124999999903189, -3.661942331401731199 ) ) ;
#7427=CARTESIAN_POINT ( 'NONE',  ( 3.291357201573688496, -4.921088562373032715, 1.760366434726516660 ) ) ;
#7429=CARTESIAN_POINT ( 'NONE',  ( 2.949251946438511407, -1.475624999999980647, 2.418581166398158455 ) ) ;
#7444=CARTESIAN_POINT ( 'NONE',  ( -3.319861881881159604, -3.147500000000079456, 1.374129751973758529 ) ) ;
#7447=FACE_OUTER_BOUND ( 'NONE', #6701, .T. ) ;
#7449=CARTESIAN_POINT ( 'NONE',  ( 2.674318815604713073, -5.110407362173572388, -2.536235381543390677 ) ) ;
#7452=CARTESIAN_POINT ( 'NONE',  ( 3.800285711464508331, -0.4995676945082491160, -1.326881515511059817 ) ) ;
#7457=DIRECTION ( 'NONE',  ( -1.000000000000000000, -1.084202172485497334E-15, 0.000000000000000000 ) ) ;
#7464=CARTESIAN_POINT ( 'NONE',  ( -2.381388125886219509, -1.944375000000168052, -2.899558211763606064 ) ) ;
#7468=CARTESIAN_POINT ( 'NONE',  ( -3.898923295066525352, -3.515625000000077716, 0.3854469994812330658 ) ) ;
#7473=CARTESIAN_POINT ( 'NONE',  ( -2.801070059014840741, 1.881841424954886710, -4.148404342226347019 ) ) ;
#7474=CARTESIAN_POINT ( 'NONE',  ( 2.431404194366990623, 4.650702586819541295, 2.977611364064985881E-16 ) ) ;
#7475=CARTESIAN_POINT ( 'NONE',  ( 3.173335668876534843, -5.499999999999995559, 3.886215369509756487E-16 ) ) ;
#7476=DIRECTION ( 'NONE',  ( 0.5000000000000002220, 0.000000000000000000, 0.8660254037844384856 ) ) ;
#7479=VERTEX_POINT ( 'NONE', #4290 ) ;
#7481=ORIENTED_EDGE ( 'NONE', *, *, #13702, .F. ) ;
#7487=CARTESIAN_POINT ( 'NONE',  ( -2.834780744084784310, -6.006874999999924469, -1.516137112471814596 ) ) ;
#7492=CIRCLE ( 'NONE', #775, 2.431404194366992400 ) ;
#7497=ORIENTED_EDGE ( 'NONE', *, *, #8487, .F. ) ;
#7498=DIRECTION ( 'NONE',  ( -2.551930889570660354E-15, 1.000000000000000000, 0.000000000000000000 ) ) ;
#7502=CARTESIAN_POINT ( 'NONE',  ( -3.144577161339557669, -2.390624999999865885, -2.578777943664209982 ) ) ;
#7503=EDGE_LOOP ( 'NONE', ( #6080, #1700, #2191 ) ) ;
#7505=CARTESIAN_POINT ( 'NONE',  ( -3.840936051835830423, -3.530463562373013175, 0.7654668794366149553 ) ) ;
#7516=VECTOR ( 'NONE', #14615, 1000.000000000000000 ) ;
#7523=CARTESIAN_POINT ( 'NONE',  ( 0.7342756466162191353, -1.803750000000060361, -3.698544502508175569 ) ) ;
#7528=CARTESIAN_POINT ( 'NONE',  ( -1.919346139099063597, -5.205827266973400036, -3.000085783918466031 ) ) ;
#7548=CARTESIAN_POINT ( 'NONE',  ( 3.722330097189530562, -1.616249999999942899, -0.7418360188101028596 ) ) ;
#7549=CARTESIAN_POINT ( 'NONE',  ( 2.153747138339810796, -3.843749999999965361, 3.220761568642789729 ) ) ;
#7561=EDGE_LOOP ( 'NONE', ( #6438, #3937, #14579, #3782 ) ) ;
#7569=CARTESIAN_POINT ( 'NONE',  ( 3.252598188045254357, -5.600624999999989306, -0.3215848719029839042 ) ) ;
#7582=CARTESIAN_POINT ( 'NONE',  ( 3.091873775341146491, -2.890625000000027534, 2.538798244104332191 ) ) ;
#7592=( GEOMETRIC_REPRESENTATION_CONTEXT ( 3 ) GLOBAL_UNCERTAINTY_ASSIGNED_CONTEXT ( ( #7785 ) ) GLOBAL_UNIT_ASSIGNED_CONTEXT ( ( #348, #433, #2832 ) ) REPRESENTATION_CONTEXT ( 'NONE', 'WORKASPACE' ) );
#7600=CARTESIAN_POINT ( 'NONE',  ( -2.441443777772109414, -1.225625000000065912, 2.973322847374054501 ) ) ;
#7608=CARTESIAN_POINT ( 'NONE',  ( -0.3198136352484399758, -0.4995676945082599407, -4.144957434285039710 ) ) ;
#7623=CARTESIAN_POINT ( 'NONE',  ( -3.717546150574369879, -2.069374999999891607, -0.3671215460811757536 ) ) ;
#7624=LINE ( 'NONE', #13589, #9044 ) ;
#7627=CARTESIAN_POINT ( 'NONE',  ( -3.771471614353887336, -4.484375000000117240, -0.3724498170710106582 ) ) ;
#7630=DIRECTION ( 'NONE',  ( -1.000000000000000000, 0.000000000000000000, 0.000000000000000000 ) ) ;
#7632=LINE ( 'NONE', #14662, #15294 ) ;
#7633=CARTESIAN_POINT ( 'NONE',  ( -1.962865815818235271, -1.671875000000012879, 3.669921287786785502 ) ) ;
#7638=FACE_OUTER_BOUND ( 'NONE', #7350, .T. ) ;
#7644=CARTESIAN_POINT ( 'NONE',  ( -0.9391448502757393513, -5.881874999999767262, -3.091762488354311778 ) ) ;
#7661=CARTESIAN_POINT ( 'NONE',  ( 0.3862366009532263167, -3.234374999999897859, -3.936230821419137271 ) ) ;
#7672=AXIS2_PLACEMENT_3D ( 'NONE', #1747, #6497, #8505 ) ;
#7676=CARTESIAN_POINT ( 'NONE',  ( -3.865847815970003598, -1.085000000000063469, -0.001011349278449839070 ) ) ;
#7679=CARTESIAN_POINT ( 'NONE',  ( -3.466497813382189541, -5.275048774667015827, -7.182839392716466875E-16 ) ) ;
#7680=CARTESIAN_POINT ( 'NONE',  ( 3.031088913245533423, 0.04639863247564009890, -3.749999999999999556 ) ) ;
#7685=ORIENTED_EDGE ( 'NONE', *, *, #5839, .F. ) ;
#7696=CARTESIAN_POINT ( 'NONE',  ( -0.3756913567350075311, -4.265625000000119904, -3.800190021185207545 ) ) ;
#7697=FACE_OUTER_BOUND ( 'NONE', #7561, .T. ) ;
#7700=CARTESIAN_POINT ( 'NONE',  ( 2.374332146000840194, -0.8437500000000230926, 3.550666350934340354 ) ) ;
#7707=ORIENTED_EDGE ( 'NONE', *, *, #12108, .F. ) ;
#7711=CARTESIAN_POINT ( 'NONE',  ( -2.276987973263394416, -5.960000000000099440, -2.278132229539954867 ) ) ;
#7714=DIRECTION ( 'NONE',  ( -1.747085166004344019E-15, 1.000000000000000000, -0.000000000000000000 ) ) ;
#7720=PLANE ( 'NONE',  #12327 ) ;
#7724=FACE_OUTER_BOUND ( 'NONE', #3723, .T. ) ;
#7725=CARTESIAN_POINT ( 'NONE',  ( 3.946741062051739579, -1.953124999999941380, 1.198372487375103157 ) ) ;
#7734=CARTESIAN_POINT ( 'NONE',  ( -0.4546285098678428671, 2.357490090293554275, 4.500000000000001776 ) ) ;
#7735=ADVANCED_FACE ( 'NONE', ( #1101 ), #1962, .F. ) ;
#7745=CARTESIAN_POINT ( 'NONE',  ( -2.746234728672138026, -0.9599999999999920819, -2.744228674164193471 ) ) ;
#7746=ORIENTED_EDGE ( 'NONE', *, *, #53, .F. ) ;
#7748=AXIS2_PLACEMENT_3D ( 'NONE', #9219, #1077, #10620 ) ;
#7753=CARTESIAN_POINT ( 'NONE',  ( -0.8000000000000104805, 8.384405323238834029, 0.000000000000000000 ) ) ;
#7768=CARTESIAN_POINT ( 'NONE',  ( -3.581950731666862175, -5.530463562373103770, 0.7115315330189105891 ) ) ;
#7769=CARTESIAN_POINT ( 'NONE',  ( -0.001042462806609206153, -0.3350000000001150946, 3.965061882346304412 ) ) ;
#7771=CARTESIAN_POINT ( 'NONE',  ( 4.096389842826703820, -2.015625000000050182, -0.4049582849837481402 ) ) ;
#7775=CARTESIAN_POINT ( 'NONE',  ( 3.275404563695782034, -1.109375000000065503, -2.686596450795923463 ) ) ;
#7779=DIRECTION ( 'NONE',  ( -1.000000000000000000, 0.000000000000000000, 0.000000000000000000 ) ) ;
#7785=UNCERTAINTY_MEASURE_WITH_UNIT (LENGTH_MEASURE( 1.000000000000000082E-05 ), #348, 'distance_accuracy_value', 'NONE');
#7796=CARTESIAN_POINT ( 'NONE',  ( 2.937061643673781752, -5.103115294876279684, -2.234448363260541193 ) ) ;
#7803=CARTESIAN_POINT ( 'NONE',  ( -0.7718104722664602679, -3.281249999999995115, -3.872775259196827857 ) ) ;
#7810=CARTESIAN_POINT ( 'NONE',  ( -3.173335668876506421, -5.500000000000010658, 0.000000000000000000 ) ) ;
#7817=CARTESIAN_POINT ( 'NONE',  ( 3.779448512589508979, -1.600625000000089226, -0.3712484392070567463 ) ) ;
#7844=CARTESIAN_POINT ( 'NONE',  ( 2.807699568699258297, -3.124999999999853895, -2.806223270957961091 ) ) ;
#7845=CYLINDRICAL_SURFACE ( 'NONE', #12969, 0.8000000000000113687 ) ;
#7848=CARTESIAN_POINT ( 'NONE',  ( 3.008642795497740607, 2.054436331234742230, 3.788877816371843288 ) ) ;
#7849=CARTESIAN_POINT ( 'NONE',  ( -3.245221319803801130, -1.390624999999827915, -2.664727821046819489 ) ) ;
#7855=DIRECTION ( 'NONE',  ( -6.982962677686266711E-15, -6.579622859988665673E-30, -1.000000000000000000 ) ) ;
#7861=AXIS2_PLACEMENT_3D ( 'NONE', #9523, #14038, #11635 ) ;
#7863=DIRECTION ( 'NONE',  ( -1.000000000000000000, 0.000000000000000000, 0.000000000000000000 ) ) ;
#7868=CARTESIAN_POINT ( 'NONE',  ( -1.266249875242109413, -5.272499999999733511, 3.060236832100306614 ) ) ;
#7875=CARTESIAN_POINT ( 'NONE',  ( -0.4212280308283230523, -0.7343750000000048850, 4.265137983724988757 ) ) ;
#7877=CARTESIAN_POINT ( 'NONE',  ( -2.584068721321989948, -2.358588562373262754, -3.146367359111198247 ) ) ;
#7889=CARTESIAN_POINT ( 'NONE',  ( 3.258191480560295616, -0.6787499999999294653, -2.178773987163739267 ) ) ;
#7893=EDGE_CURVE ( 'NONE', #160, #6471, #1416, .T. ) ;
#7896=CARTESIAN_POINT ( 'NONE',  ( 3.867986884670384207, -0.4995676945082496712, 0.8486844468283908371 ) ) ;
#7901=VERTEX_POINT ( 'NONE', #14290 ) ;
#7907=CARTESIAN_POINT ( 'NONE',  ( 3.308479819675366862, -6.061713562373198805, -1.371850503680594802 ) ) ;
#7910=CARTESIAN_POINT ( 'NONE',  ( 3.689984836354881281, -2.937500000000126565, 1.529580092797385715 ) ) ;
#7914=CARTESIAN_POINT ( 'NONE',  ( -4.184567129761759929, -1.500000000000142109, 0.001513272625389735625 ) ) ;
#7918=ADVANCED_FACE ( 'NONE', ( #6240 ), #10848, .T. ) ;
#7927=CARTESIAN_POINT ( 'NONE',  ( -3.313940955170693758, -4.131874999999921805, 1.004348227522835924 ) ) ;
#7930=CARTESIAN_POINT ( 'NONE',  ( 4.763139720814411504, 0.04639863247564429694, 0.7499999999999985567 ) ) ;
#7931=DIRECTION ( 'NONE',  ( 0.000000000000000000, 0.000000000000000000, 1.000000000000000000 ) ) ;
#7934=CARTESIAN_POINT ( 'NONE',  ( 1.624300153006762448, -0.4995676945082549447, 3.676067300042933805 ) ) ;
#7937=CARTESIAN_POINT ( 'NONE',  ( 2.931584255716234821, -5.103127331515293186, -2.242088070657691556 ) ) ;
#7941=CARTESIAN_POINT ( 'NONE',  ( -4.316892141304113473, -0.5000000000000647260, -0.001152797426451617618 ) ) ;
#7943=CARTESIAN_POINT ( 'NONE',  ( -3.872011465033448285, -2.546088562373184150, 1.176098017510569305 ) ) ;
#7946=CARTESIAN_POINT ( 'NONE',  ( -1.006616814747114486E-29, -2.568816543514388222E-44, -4.500000000000000888 ) ) ;
#7954=CARTESIAN_POINT ( 'NONE',  ( 3.639928100339127948, -0.5225000000000105116, 1.508827519571796394 ) ) ;
#7956=CARTESIAN_POINT ( 'NONE',  ( -3.535952561574606801, -3.053750000000104770, -0.7042925846621640451 ) ) ;
#7961=CIRCLE ( 'NONE', #6015, 0.8000000000000176970 ) ;
#7972=CARTESIAN_POINT ( 'NONE',  ( -0.3378546177656731597, -4.319374999999974207, 3.421346328963576156 ) ) ;
#7976=CARTESIAN_POINT ( 'NONE',  ( -3.504929897947095530, -5.452338562372976760, -1.061798670046178783 ) ) ;
#7978=CARTESIAN_POINT ( 'NONE',  ( 3.768993168962329054, -0.5381249999999744293, 1.141810966380977455 ) ) ;
#7980=CARTESIAN_POINT ( 'NONE',  ( -0.7951559085591690668, -2.281249999999988010, -4.003048974988245412 ) ) ;
#7996=CARTESIAN_POINT ( 'NONE',  ( 1.614039610742502573, -4.413124999999970655, 3.021508266705727586 ) ) ;
#7999=DIRECTION ( 'NONE',  ( 0.000000000000000000, 0.000000000000000000, -1.000000000000000000 ) ) ;
#8004=CARTESIAN_POINT ( 'NONE',  ( -4.278680128878765032, -0.4995676945082698217, 0.4731733880612277177 ) ) ;
#8008=VERTEX_POINT ( 'NONE', #5376 ) ;
#8010=EDGE_CURVE ( 'NONE', #13047, #3975, #7632, .T. ) ;
#8018=CARTESIAN_POINT ( 'NONE',  ( 3.919974135967671636, -1.062500000000018652, -1.622483930095183213 ) ) ;
#8020=CARTESIAN_POINT ( 'NONE',  ( -3.380984900159444528, -2.405463562373173936, -2.257326875190593274 ) ) ;
#8029=DIRECTION ( 'NONE',  ( -2.551930889570659960E-15, 1.000000000000000000, 0.000000000000000000 ) ) ;
#8033=CARTESIAN_POINT ( 'NONE',  ( 0.3809421545653357000, -0.8193749999999933031, -3.882302026224181635 ) ) ;
#8035=AXIS2_PLACEMENT_3D ( 'NONE', #13408, #11080, #11149 ) ;
#8038=CARTESIAN_POINT ( 'NONE',  ( 1.055499318045234114, -2.788125000000055476, -3.484140247641438926 ) ) ;
#8040=DIRECTION ( 'NONE',  ( -1.000000000000000000, -1.724434379501977811E-15, 0.000000000000000000 ) ) ;
#8051=CARTESIAN_POINT ( 'NONE',  ( 3.388605160257775584, -4.569374999999831211, 0.3324735777646721790 ) ) ;
#8055=CARTESIAN_POINT ( 'NONE',  ( -3.506906588862749086, -6.499213562373093112, 0.000000000000000000 ) ) ;
#8056=CARTESIAN_POINT ( 'NONE',  ( -2.210630411551929075, -0.2412499999998789502, 3.306558829207901340 ) ) ;
#8060=CARTESIAN_POINT ( 'NONE',  ( 3.905735209131758534, -3.031249999999969802, -0.7758307200683374205 ) ) ;
#8062=EDGE_CURVE ( 'NONE', #502, #13047, #6611, .T. ) ;
#8063=CARTESIAN_POINT ( 'NONE',  ( -4.785585838562203875, 2.054436331234722246, 0.7111221836281561570 ) ) ;
#8065=CARTESIAN_POINT ( 'NONE',  ( 4.296275033669349597, -0.4995676945082477838, 5.261419468239855985E-16 ) ) ;
#8078=CARTESIAN_POINT ( 'NONE',  ( -2.669536895096369378, -4.194375000000057696, 2.192493760422927984 ) ) ;
#8098=CARTESIAN_POINT ( 'NONE',  ( 2.351042318464003689, -1.156249999999995559, -3.516557504029556913 ) ) ;
#8101=CARTESIAN_POINT ( 'NONE',  ( 3.986784942675642540, -2.999213562373096220, 0.001049275647879016615 ) ) ;
#8105=ADVANCED_FACE ( 'NONE', ( #5146 ), #4671, .T. ) ;
#8117=CARTESIAN_POINT ( 'NONE',  ( 1.493882881115754069, -0.7724999999999562217, -3.610279343491855641 ) ) ;
#8121=CARTESIAN_POINT ( 'NONE',  ( 1.740706783794652379, -2.413124999999917808, 3.253752085064650412 ) ) ;
#8132=VERTEX_POINT ( 'NONE', #3409 ) ;
#8136=CARTESIAN_POINT ( 'NONE',  ( 2.991299100910195463, -4.663125000000096776, -1.600316903339956687 ) ) ;
#8140=CARTESIAN_POINT ( 'NONE',  ( 0.7473096651600278362, -4.217963562373095776, -3.751860142188157887 ) ) ;
#8142=CONICAL_SURFACE ( 'NONE', #708, 4.500000000000000888, 1.396263401595466691 ) ;
#8145=CARTESIAN_POINT ( 'NONE',  ( -4.015299829665333498, 2.374507716408090996, 2.045296687396993107 ) ) ;
#8146=CARTESIAN_POINT ( 'NONE',  ( -4.296391350416484123, -0.4995676945082700438, -1.627175273956673067E-05 ) ) ;
#8149=DIRECTION ( 'NONE',  ( -1.000000000000000000, 0.000000000000000000, 1.669238443041288662E-16 ) ) ;
#8150=CARTESIAN_POINT ( 'NONE',  ( 3.341349309646173715, -4.553750000000432507, 0.6655201449779497569 ) ) ;
#8157=ORIENTED_EDGE ( 'NONE', *, *, #673, .T. ) ;
#8158=CARTESIAN_POINT ( 'NONE',  ( 3.341349309646173715, -4.553750000000432507, 0.6655201449779497569 ) ) ;
#8169=EDGE_CURVE ( 'NONE', #6270, #8371, #114, .T. ) ;
#8171=ORIENTED_EDGE ( 'NONE', *, *, #5650, .T. ) ;
#8172=CARTESIAN_POINT ( 'NONE',  ( 0.000000000000000000, 0.000000000000000000, 0.000000000000000000 ) ) ;
#8175=CARTESIAN_POINT ( 'NONE',  ( 0.8338062855310036658, -0.7812499999999443778, 4.197676506703500010 ) ) ;
#8177=CARTESIAN_POINT ( 'NONE',  ( -1.147267920495149918, -3.296088562373144182, -3.777078554815655131 ) ) ;
#8180=CARTESIAN_POINT ( 'NONE',  ( 4.015299829665321063, 2.374507716408110536, -2.045296687396993107 ) ) ;
#8185=FACE_OUTER_BOUND ( 'NONE', #10180, .T. ) ;
#8188=CARTESIAN_POINT ( 'NONE',  ( 2.644209610478730266, -4.874999999999846345, 2.642267524923772370 ) ) ;
#8190=CARTESIAN_POINT ( 'NONE',  ( -0.001340710925747373022, -2.834999999999994635, -3.634308738048381393 ) ) ;
#8192=EDGE_CURVE ( 'NONE', #8567, #6471, #11392, .T. ) ;
#8212=CARTESIAN_POINT ( 'NONE',  ( 3.390724153796742968, -4.077338562372932351, -1.811240771910064051 ) ) ;
#8215=CARTESIAN_POINT ( 'NONE',  ( -3.452158817763116616, 2.307268873417411381, 3.020685531837380200 ) ) ;
#8221=DIRECTION ( 'NONE',  ( -1.000000000000000000, -2.548822376660340629E-15, 0.000000000000000000 ) ) ;
#8223=CARTESIAN_POINT ( 'NONE',  ( -2.533829858540697977, -3.209999999999945786, 2.535703909530142575 ) ) ;
#8233=CARTESIAN_POINT ( 'NONE',  ( 1.394838545734166990, -2.772499999999996856, -3.364978284447634582 ) ) ;
#8235=CARTESIAN_POINT ( 'NONE',  ( 4.330127018922192761, 1.086454989718688594E-14, 1.499999999999999112 ) ) ;
#8236=CARTESIAN_POINT ( 'NONE',  ( 3.654380903460823671, -4.968749999999916511, 0.7255053565382596492 ) ) ;
#8248=CARTESIAN_POINT ( 'NONE',  ( -4.427870617159052280, 0.4999999999999987232, -3.710358631349437542E-13 ) ) ;
#8251=CARTESIAN_POINT ( 'NONE',  ( -3.470181165153897407, -1.592963562373082897, 2.317368808847834583 ) ) ;
#8268=CARTESIAN_POINT ( 'NONE',  ( 2.968551569176787197, -4.109374999999867661, -2.434929705433495073 ) ) ;
#8271=CARTESIAN_POINT ( 'NONE',  ( -3.335258087793214088, -3.022499999999893827, -1.380066378191329379 ) ) ;
#8279=DIRECTION ( 'NONE',  ( -1.000000000000000000, -2.551930889570659565E-15, 0.000000000000000000 ) ) ;
#8287=ORIENTED_EDGE ( 'NONE', *, *, #673, .F. ) ;
#8290=CARTESIAN_POINT ( 'NONE',  ( 3.682145644596256151, -4.046088562373215680, -1.118437823483080296 ) ) ;
#8295=CARTESIAN_POINT ( 'NONE',  ( -3.250000000000014211, 7.362499999999993605, 3.980102097228917460E-16 ) ) ;
#8299=CARTESIAN_POINT ( 'NONE',  ( -0.8655643756567900082, -2.325867345846483398E-15, 4.500000000000000000 ) ) ;
#8303=CARTESIAN_POINT ( 'NONE',  ( 1.363531154075378282, -3.397500000000037712, 3.288412936073061399 ) ) ;
#8305=ORIENTED_EDGE ( 'NONE', *, *, #13080, .T. ) ;
#8309=ORIENTED_EDGE ( 'NONE', *, *, #14835, .T. ) ;
#8315=CARTESIAN_POINT ( 'NONE',  ( 2.950365215318619949, -3.491249999999835651, 1.969791294043586660 ) ) ;
#8323=AXIS2_PLACEMENT_3D ( 'NONE', #10885, #6243, #7476 ) ;
#8336=CARTESIAN_POINT ( 'NONE',  ( -1.660422764420820929, -0.3125000000000191513, -4.011647887856864436 ) ) ;
#8338=CIRCLE ( 'NONE', #14274, 2.577850803773722443 ) ;
#8339=CARTESIAN_POINT ( 'NONE',  ( -0.001142616198797753811, -0.7492135623732086858, 4.284427141808827777 ) ) ;
#8353=CARTESIAN_POINT ( 'NONE',  ( 2.130457310823663519, -4.156249999999911182, -3.186652721750134809 ) ) ;
#8357=CARTESIAN_POINT ( 'NONE',  ( -0.3768771888557862493, -1.319375000000004405, 3.816279424444235069 ) ) ;
#8360=DIRECTION ( 'NONE',  ( -2.551930889570659960E-15, 1.000000000000000000, 0.000000000000000000 ) ) ;
#8369=CARTESIAN_POINT ( 'NONE',  ( -1.990045403832507054, -3.241250000000046594, 2.976654046991287217 ) ) ;
#8371=VERTEX_POINT ( 'NONE', #3646 ) ;
#8372=EDGE_CURVE ( 'NONE', #12263, #2643, #11411, .T. ) ;
#8382=CARTESIAN_POINT ( 'NONE',  ( -3.313940955170693758, -4.131874999999921805, 1.004348227522835924 ) ) ;
#8387=ORIENTED_EDGE ( 'NONE', *, *, #1449, .T. ) ;
#8392=CARTESIAN_POINT ( 'NONE',  ( 1.766265845880009788, -4.828125000000014211, 3.301533676270316686 ) ) ;
#8394=CARTESIAN_POINT ( 'NONE',  ( -0.8000000000000111466, 9.015594676761164550, 0.000000000000000000 ) ) ;
#8406=VERTEX_POINT ( 'NONE', #145 ) ;
#8411=CARTESIAN_POINT ( 'NONE',  ( -0.4082801294501576805, -1.733588562373098663, 4.134097036138766335 ) ) ;
#8422=CARTESIAN_POINT ( 'NONE',  ( -1.438726384651785040, -4.687499999999733546, 3.477001582427886817 ) ) ;
#8424=CARTESIAN_POINT ( 'NONE',  ( -3.693744850241972077, -1.131875000000025722, 1.119430425315776523 ) ) ;
#8434=CARTESIAN_POINT ( 'NONE',  ( 3.389189273868537189, -3.538124999999807674, 1.026728768593258012 ) ) ;
#8435=ORIENTED_EDGE ( 'NONE', *, *, #8440, .T. ) ;
#8440=EDGE_CURVE ( 'NONE', #14968, #3175, #2549, .T. ) ;
#8445=CARTESIAN_POINT ( 'NONE',  ( 1.403561989263864891E-14, -5.500000000000007994, 0.000000000000000000 ) ) ;
#8447=CARTESIAN_POINT ( 'NONE',  ( -0.9979582191391829227, -4.288125000000008846, 3.294238300096191452 ) ) ;
#8458=FACE_OUTER_BOUND ( 'NONE', #2910, .T. ) ;
#8463=DIRECTION ( 'NONE',  ( -1.000000000000000000, -1.084202172485497334E-15, 0.000000000000000000 ) ) ;
#8469=EDGE_LOOP ( 'NONE', ( #14275, #15291, #14707, #14823, #6654 ) ) ;
#8474=DIRECTION ( 'NONE',  ( -9.422394424380278809E-16, 1.000000000000000000, -0.000000000000000000 ) ) ;
#8477=CARTESIAN_POINT ( 'NONE',  ( 4.200656737305518362, 0.04687500000002611800, 1.272606865360604189 ) ) ;
#8479=CARTESIAN_POINT ( 'NONE',  ( -0.8351328658836442154, -0.7179635623729614391, 4.206420318747179365 ) ) ;
#8480=( GEOMETRIC_REPRESENTATION_CONTEXT ( 3 ) GLOBAL_UNCERTAINTY_ASSIGNED_CONTEXT ( ( #13377 ) ) GLOBAL_UNIT_ASSIGNED_CONTEXT ( ( #11146, #1609, #4091 ) ) REPRESENTATION_CONTEXT ( 'NONE', 'WORKASPACE' ) );
#8487=EDGE_CURVE ( 'NONE', #9386, #7247, #1696, .T. ) ;
#8496=CARTESIAN_POINT ( 'NONE',  ( 1.826535687659961660, -3.828124999999970246, 3.419360526609917628 ) ) ;
#8499=CARTESIAN_POINT ( 'NONE',  ( 3.931950937192209228, -0.5849999999998678479, -0.001434051515494208940 ) ) ;
#8500=EDGE_CURVE ( 'NONE', #8132, #4034, #5874, .T. ) ;
#8505=DIRECTION ( 'NONE',  ( -1.000000000000000000, -2.551930889570659960E-15, 0.000000000000000000 ) ) ;
#8514=CARTESIAN_POINT ( 'NONE',  ( 3.601230736643933117, -2.553749999999958220, 0.7149504581460883745 ) ) ;
#8527=CARTESIAN_POINT ( 'NONE',  ( 0.3508518002069317410, -3.350624999999907150, 3.548798009676430887 ) ) ;
#8537=CARTESIAN_POINT ( 'NONE',  ( 0.6849063648203621568, -3.803749999999915143, -3.438650935610223947 ) ) ;
#8542=CARTESIAN_POINT ( 'NONE',  ( 2.598076211353315124, 0.1227504548087477720, 4.500000000000000000 ) ) ;
#8546=DIRECTION ( 'NONE',  ( 1.000000000000000000, 2.459952698498907718E-15, 0.000000000000000000 ) ) ;
#8554=CARTESIAN_POINT ( 'NONE',  ( -3.189069343666966816, -6.084999999999998188, 0.000000000000000000 ) ) ;
#8556=CARTESIAN_POINT ( 'NONE',  ( -3.599033699595752367, -0.4062500000000055511, -2.406188570379728553 ) ) ;
#8557=CARTESIAN_POINT ( 'NONE',  ( 2.301140841363210399, -1.842963562373116204, 3.441202151216794292 ) ) ;
#8564=DIRECTION ( 'NONE',  ( -9.422394424380278809E-16, 1.000000000000000000, -0.000000000000000000 ) ) ;
#8567=VERTEX_POINT ( 'NONE', #3087 ) ;
#8568=CARTESIAN_POINT ( 'NONE',  ( 0.000000000000000000, 0.000000000000000000, 0.000000000000000000 ) ) ;
#8574=CARTESIAN_POINT ( 'NONE',  ( -3.630950894689927821, -4.453124999999883649, -1.099983568547476143 ) ) ;
#8576=CARTESIAN_POINT ( 'NONE',  ( 3.193773564512591090, -4.092963562373205022, -2.135702085600666322 ) ) ;
#8586=ADVANCED_FACE ( 'NONE', ( #10129 ), #8142, .T. ) ;
#8592=VERTEX_POINT ( 'NONE', #14860 ) ;
#8596=CARTESIAN_POINT ( 'NONE',  ( 1.055499318045256540, -2.788125000000055476, -3.484140247641439370 ) ) ;
#8603=CARTESIAN_POINT ( 'NONE',  ( -2.729504910555624608, -5.227506838825849655, -2.243639822945930007 ) ) ;
#8605=CARTESIAN_POINT ( 'NONE',  ( -2.123244931150037651, -0.4995676945082646037, -3.627165614345276179 ) ) ;
#8617=CARTESIAN_POINT ( 'NONE',  ( -0.3862366009529625832, -3.265625000000082601, -3.932116680993492874 ) ) ;
#8622=DIRECTION ( 'NONE',  ( 2.551930889570659960E-15, -1.000000000000000000, -0.000000000000000000 ) ) ;
#8630=CARTESIAN_POINT ( 'NONE',  ( 3.252598188045254801, -5.600624999999989306, -0.3215848719029840153 ) ) ;
#8632=CARTESIAN_POINT ( 'NONE',  ( 3.013463120154616703, -5.647500000000105658, -1.249542180252701584 ) ) ;
#8646=CARTESIAN_POINT ( 'NONE',  ( 3.303237764219515427, -3.093750000000110578, -2.208893390251179589 ) ) ;
#8648=CARTESIAN_POINT ( 'NONE',  ( -3.788356809919846580, -4.499213562373157060, -0.0009870486262349110682 ) ) ;
#8649=CARTESIAN_POINT ( 'NONE',  ( -1.470831194960214861, -1.272500000000085230, 3.548278161707651090 ) ) ;
#8663=DIRECTION ( 'NONE',  ( -1.000000000000000000, 0.000000000000000000, 0.000000000000000000 ) ) ;
#8664=CARTESIAN_POINT ( 'NONE',  ( 1.033118776976111652, -3.381875000000070131, 3.408891928937247240 ) ) ;
#8667=CARTESIAN_POINT ( 'NONE',  ( -1.336190917661197242, -3.897499999999990195, -3.228188129988408317 ) ) ;
#8672=ADVANCED_FACE ( 'NONE', ( #4875 ), #7172, .T. ) ;
#8674=DIRECTION ( 'NONE',  ( -1.000000000000000000, -2.551930889570659960E-15, 0.000000000000000000 ) ) ;
#8680=ORIENTED_EDGE ( 'NONE', *, *, #4976, .T. ) ;
#8682=VERTEX_POINT ( 'NONE', #2529 ) ;
#8688=CARTESIAN_POINT ( 'NONE',  ( 2.337649614532405717, -2.444375000000051479, 2.849939602875970035 ) ) ;
#8690=CARTESIAN_POINT ( 'NONE',  ( -2.667345689317278890, -4.625000000000156319, 2.665957393838279010 ) ) ;
#8693=CYLINDRICAL_SURFACE ( 'NONE', #11061, 0.8000000000000113687 ) ;
#8694=DIRECTION ( 'NONE',  ( 1.000000000000000000, 1.067522139062645347E-15, 0.000000000000000000 ) ) ;
#8705=CARTESIAN_POINT ( 'NONE',  ( -2.276987973263314480, -5.960000000000099440, -2.278132229539954867 ) ) ;
#8707=CARTESIAN_POINT ( 'NONE',  ( 1.804507757947478197, -5.741250000000162501, -2.702832914148806331 ) ) ;
#8718=DIRECTION ( 'NONE',  ( 9.422394424380278809E-16, -1.000000000000000000, 0.000000000000000000 ) ) ;
#8721=CARTESIAN_POINT ( 'NONE',  ( -1.629699455448989389E-14, 8.699999999999999289, 5.655858585055787181E-29 ) ) ;
#8722=CARTESIAN_POINT ( 'NONE',  ( -4.034970194612536254, -2.484375000000152767, -0.3959303163385184399 ) ) ;
#8724=CARTESIAN_POINT ( 'NONE',  ( -3.020162574906126274, -3.608588562373100661, 2.477258684347839246 ) ) ;
#8726=EDGE_CURVE ( 'NONE', #13967, #160, #12115, .T. ) ;
#8727=DIRECTION ( 'NONE',  ( -9.422394424380274864E-16, 1.000000000000000000, -0.000000000000000000 ) ) ;
#8741=CARTESIAN_POINT ( 'NONE',  ( -2.381388125886219509, -1.944375000000168052, -2.899558211763606508 ) ) ;
#8747=CARTESIAN_POINT ( 'NONE',  ( 2.919796888921922573, -5.104126807837104707, -2.256669152708658643 ) ) ;
#8748=CARTESIAN_POINT ( 'NONE',  ( -5.196152422706630247, 0.1227504548087275521, -7.569115911492098221E-16 ) ) ;
#8752=DIRECTION ( 'NONE',  ( -1.000000000000000000, -2.622621077317916910E-15, 0.000000000000000000 ) ) ;
#8762=ORIENTED_EDGE ( 'NONE', *, *, #4976, .F. ) ;
#8767=CARTESIAN_POINT ( 'NONE',  ( -3.657957510581538507, -2.116249999999859632, 0.7266254446581354998 ) ) ;
#8771=CARTESIAN_POINT ( 'NONE',  ( -2.415777803760090325, -4.359374999999756639, -2.941435367455751848 ) ) ;
#8777=CARTESIAN_POINT ( 'NONE',  ( -4.293030807686615269, -0.5110219675973943776, 0.2974983986620418630 ) ) ;
#8780=ADVANCED_FACE ( 'NONE', ( #15244 ), #6425, .T. ) ;
#8785=ORIENTED_EDGE ( 'NONE', *, *, #14616, .T. ) ;
#8786=CARTESIAN_POINT ( 'NONE',  ( -2.488972454571051429, -5.975625000000068354, -2.041081048424583155 ) ) ;
#8796=CARTESIAN_POINT ( 'NONE',  ( 0.8000000000000175859, 9.500000000000000000, 9.797174393179039389E-17 ) ) ;
#8801=B_SPLINE_SURFACE_WITH_KNOTS ( 'NONE', 1, 3, ( 
 ( #8554, #6329, #12364, #1501, #9064, #8786, #8705, #325, #13302, #5071, #14597, #1575, #11389, #3976, #4341, #5156, #9787, #12634, #14519, #13454, #14948, #8630, #12132, #248, #2816, #9866, #2897, #6405, #1655, #4993, #1725, #3172, #6252, #13378, #12286, #14442, #754, #5513, #413, #11041, #9707, #11117, #3827, #2663, #7409, #2734, #489, #10213, #5224, #9939, #10443, #6906, #11698, #5676, #10371, #12946, #4482, #987, #10297, #3239, #3320, #8136, #1147, #14026, #9204, #8051, #10607, #5740, #15172, #4722, #9288, #11549, #13945, #837, #15329, #2306, #7972, #3400, #12870, #7058, #9366, #2230, #6973, #1062, #12707, #10526, #4650, #2079, #3474, #6829, #13028, #5592, #11777, #9437, #3551, #916, #9663, #56, #10773, #280, #3707, #12094, #210, #5030, #11932, #4955, #6059, #9591, #7210, #8434, #10682, #9747, #9829, #14254, #13179, #1299, #8664, #2540, #14561, #6213, #6289, #2622, #8369, #2460, #7370, #14330, #7444, #12158, #7290, #3943, #12016, #14395, #3784, #5981, #11000, #2387, #14482, #4801, #13112, #1461, #3869, #8596, #7138, #1384, #11857, #132, #6141, #10850, #9515, #369, #4885, #8514, #10921, #13342, #2699, #1532, #5117, #1222, #3636, #11375, #6666, #12241, #4175, #6442, #5340, #6588, #741, #454, #12325, #522, #1914, #5496, #14627, #12399, #10198, #3082, #14931, #8741, #590, #2770, #4012, #13569, #11081, #7523, #1834, #8972, #13487, #1612, #4094, #6366, #14856, #12552, #7817, #2852, #3007, #1759, #8899, #4320, #11150, #13639, #8822, #11301, #1691, #13409, #4244, #5191, #13712, #9902, #7600, #5259, #670, #9976, #14706, #2935, #7676, #6509, #11224, #10054, #14786, #7745, #12473, #5423, #10124, #14009, #10426, #8033, #3385, #8117, #9187, #7037, #2288, #7889, #15154, #2064, #972, #2213, #11760, #11453, #7954, #11531, #12926, #1129, #10275, #12772, #5890, #14090, #10592, #4396, #11608, #13787, #15006, #13930, #6734, #3158, #12851, #4632, #9117, #12621 ),
 ( #1045, #2141, #9350, #6887, #5655, #11677, #13855, #10355, #15315, #3223, #5724, #3456, #15080, #6956, #5802, #4546, #819, #9045, #5574, #4467, #9269, #10507, #1984, #3302, #12691, #6812, #15236, #8188, #896, #2680, #13240, #2520, #4779, #7120, #9497, #8422, #1278, #262, #13164, #13320, #14314, #14234, #1513, #3618, #7270, #8574, #13095, #5966, #6269, #11994, #3693, #2597, #192, #10830, #10982, #10904, #7425, #36, #8353, #6123, #8268, #9728, #14465, #9573, #10750, #4706, #1360, #12144, #9417, #1207, #2446, #7196, #8496, #11916, #6042, #112, #13008, #12077, #14157, #10662, #4864, #4939, #3533, #9648, #2367, #7349, #11840, #14381, #3766, #1442, #6198, #5012, #3847, #5409, #11133, #7803, #12307, #7661, #12382, #3921, #8952, #349, #2987, #8646, #6350, #11204, #13621, #1815, #12532, #1676, #1899, #14611, #7582, #8803, #2747, #4228, #13470, #5240, #14689, #5321, #1740, #4077, #10036, #14772, #505, #13692, #3064, #14539, #6490, #8722, #572, #8883, #6653, #7502, #3991, #2833, #5093, #9807, #1595, #13555, #13391, #10110, #12220, #11064, #2918, #434, #5172, #9956, #9883, #6422, #4159, #11285, #7725, #12453, #6570, #654, #14842, #10493, #5784, #11435, #956, #15066, #6871, #4610, #4382, #2122, #6796, #4530, #10260, #1030, #2199, #11361, #6942, #11660, #9333, #9102, #11514, #11592, #13768, #5710, #13914, #3142, #878, #12608, #12905, #2271, #8098, #14072, #3286, #13991, #8018, #9029, #13843, #9253, #12675, #10409, #9172, #3365, #5557, #12755, #14988, #3442, #8175, #5481, #7875, #729, #15138, #10179, #14911, #4301, #12836, #4455, #6720, #800, #7941, #5641, #10340, #3600, #8556, #11825, #3678, #2582, #8336, #10814, #9636, #2500, #4690, #10893, #9403, #2433, #11975, #3748, #13304, #1259, #3831, #14140, #7181, #8477, #12994, #4995, #4927, #4846, #1191, #3515, #5949, #95, #13081, #7331, #14301, #250, #6025, #10647, #7018, #19, #1344, #9709, #4764, #8248 ) ),
 .UNSPECIFIED., .F., .F., .F.,
 ( 2, 2 ),
 ( 4, 2, 2, 2, 2, 2, 2, 2, 2, 2, 2, 2, 2, 2, 2, 2, 2, 2, 2, 2, 2, 2, 2, 2, 2, 2, 2, 2, 2, 2, 2, 2, 2, 2, 2, 2, 2, 2, 2, 2, 2, 2, 2, 2, 2, 2, 2, 2, 2, 2, 2, 2, 2, 2, 2, 2, 2, 2, 2, 2, 2, 2, 2, 2, 2, 2, 2, 2, 2, 2, 2, 2, 2, 2, 2, 2, 2, 2, 2, 2, 2, 2, 2, 2, 2, 2, 2, 2, 2, 2, 2, 2, 2, 2, 2, 2, 2, 2, 2, 2, 2, 2, 2, 2, 2, 2, 2, 2, 2, 2, 2, 2, 2, 2, 2, 2, 2, 2, 2, 2, 2, 2, 2, 2, 2, 2, 2, 2, 4 ),
 ( 0.000000000000000000, 1.000000000000000000 ),
 ( 0.000000000000000000, 0.007812500000000000000, 0.01562500000000000000, 0.02343750000000000000, 0.03125000000000000000, 0.03906250000000000000, 0.04687500000000000000, 0.05468750000000000000, 0.06250000000000000000, 0.07031250000000000000, 0.07812500000000000000, 0.08593750000000000000, 0.09375000000000000000, 0.1015625000000000000, 0.1093750000000000000, 0.1171875000000000000, 0.1250000000000000000, 0.1328125000000000000, 0.1406250000000000000, 0.1484375000000000000, 0.1562500000000000000, 0.1640625000000000000, 0.1718750000000000000, 0.1796875000000000000, 0.1875000000000000000, 0.1953125000000000000, 0.2031250000000000000, 0.2109375000000000000, 0.2187500000000000000, 0.2265625000000000000, 0.2343750000000000000, 0.2421875000000000000, 0.2500000000000000000, 0.2578125000000000000, 0.2656250000000000000, 0.2734375000000000000, 0.2812500000000000000, 0.2890625000000000000, 0.2968750000000000000, 0.3046875000000000000, 0.3125000000000000000, 0.3203125000000000000, 0.3281250000000000000, 0.3359375000000000000, 0.3437500000000000000, 0.3515625000000000000, 0.3593750000000000000, 0.3671875000000000000, 0.3750000000000000000, 0.3828125000000000000, 0.3906250000000000000, 0.3984375000000000000, 0.4062500000000000000, 0.4140625000000000000, 0.4218750000000000000, 0.4296875000000000000, 0.4375000000000000000, 0.4453125000000000000, 0.4531250000000000000, 0.4609375000000000000, 0.4687500000000000000, 0.4765625000000000000, 0.4843750000000000000, 0.4921875000000000000, 0.5000000000000000000, 0.5078125000000000000, 0.5156250000000000000, 0.5234375000000000000, 0.5312500000000000000, 0.5390625000000000000, 0.5468750000000000000, 0.5546875000000000000, 0.5625000000000000000, 0.5703125000000000000, 0.5781250000000000000, 0.5859375000000000000, 0.5937500000000000000, 0.6015625000000000000, 0.6093750000000000000, 0.6171875000000000000, 0.6250000000000000000, 0.6328125000000000000, 0.6406250000000000000, 0.6484375000000000000, 0.6562500000000000000, 0.6640625000000000000, 0.6718750000000000000, 0.6796875000000000000, 0.6875000000000000000, 0.6953125000000000000, 0.7031250000000000000, 0.7109375000000000000, 0.7187500000000000000, 0.7265625000000000000, 0.7343750000000000000, 0.7421875000000000000, 0.7500000000000000000, 0.7578125000000000000, 0.7656250000000000000, 0.7734375000000000000, 0.7812500000000000000, 0.7890625000000000000, 0.7968750000000000000, 0.8046875000000000000, 0.8125000000000000000, 0.8203125000000000000, 0.8281250000000000000, 0.8359375000000000000, 0.8437500000000000000, 0.8515625000000000000, 0.8593750000000000000, 0.8671875000000000000, 0.8750000000000000000, 0.8828125000000000000, 0.8906250000000000000, 0.8984375000000000000, 0.9062500000000000000, 0.9140625000000000000, 0.9218750000000000000, 0.9296875000000000000, 0.9375000000000000000, 0.9453125000000000000, 0.9531250000000000000, 0.9609375000000000000, 0.9687500000000000000, 0.9765625000000000000, 0.9843750000000000000, 0.9921875000000000000, 1.000000000000000000 ),
 .UNSPECIFIED. ) ;
#8803=CARTESIAN_POINT ( 'NONE',  ( 2.541707380700019225, -2.859374999999939160, 3.094782911937220771 ) ) ;
#8811=CARTESIAN_POINT ( 'NONE',  ( 0.000000000000000000, 0.000000000000000000, 0.000000000000000000 ) ) ;
#8822=CARTESIAN_POINT ( 'NONE',  ( 1.801006600569702520, -1.413124999999811449, 3.371562913404279271 ) ) ;
#8829=CARTESIAN_POINT ( 'NONE',  ( 2.598076211353314235, 0.1227504548087474667, -4.499999999999999112 ) ) ;
#8830=CARTESIAN_POINT ( 'NONE',  ( 3.405785683274218378, -0.4995676945082505038, -2.189026399521772248 ) ) ;
#8846=DIRECTION ( 'NONE',  ( -2.551930889570660354E-15, 1.000000000000000000, 0.000000000000000000 ) ) ;
#8848=CARTESIAN_POINT ( 'NONE',  ( 0.0009972298945177876170, -4.250000000000088818, -3.820821809411817149 ) ) ;
#8852=CARTESIAN_POINT ( 'NONE',  ( -3.873284713637146215, -1.437499999999919620, -1.605572741981209139 ) ) ;
#8866=CARTESIAN_POINT ( 'NONE',  ( 3.270563417710622645, -5.585000000000047038, 0.0008246681304769601546 ) ) ;
#8868=DIRECTION ( 'NONE',  ( 1.000000000000000000, 2.551930889570660354E-15, 0.000000000000000000 ) ) ;
#8874=EDGE_CURVE ( 'NONE', #7247, #11128, #8895, .T. ) ;
#8875=CARTESIAN_POINT ( 'NONE',  ( 1.614039610742502573, -4.413124999999970655, 3.021508266705727586 ) ) ;
#8877=FACE_BOUND ( 'NONE', #2576, .T. ) ;
#8883=CARTESIAN_POINT ( 'NONE',  ( -3.752022838101215285, -2.437499999999895195, -1.552542887664947635 ) ) ;
#8885=CARTESIAN_POINT ( 'NONE',  ( 0.3822547408368546229, -3.764838562373000741, 3.866615621364059230 ) ) ;
#8889=CARTESIAN_POINT ( 'NONE',  ( 0.8667276783653437011, 1.850460790996585685E-15, -4.499999999999999112 ) ) ;
#8895=CIRCLE ( 'NONE', #7672, 4.500000000000000888 ) ;
#8897=EDGE_LOOP ( 'NONE', ( #12671, #10663, #6649, #1089, #9290, #54 ) ) ;
#8899=CARTESIAN_POINT ( 'NONE',  ( 3.359686712366170447, -1.506874999999983755, 1.796916873358725963 ) ) ;
#8904=CARTESIAN_POINT ( 'NONE',  ( -4.244864575696460918, -0.4995676945082702658, -0.6400435777867373721 ) ) ;
#8916=CARTESIAN_POINT ( 'NONE',  ( 2.551069250243800379, -5.874213562372941233, 2.549185564325499698 ) ) ;
#8918=CARTESIAN_POINT ( 'NONE',  ( -0.7236788045118704993, -2.303749999999964437, 3.633254187536902435 ) ) ;
#8920=CARTESIAN_POINT ( 'NONE',  ( 3.568675334318531345, -3.937499999999699796, 1.476665218992084139 ) ) ;
#8925=CARTESIAN_POINT ( 'NONE',  ( -3.468190155366909888, -1.593749999999917621, 2.319185894079683230 ) ) ;
#8933=ORIENTED_EDGE ( 'NONE', *, *, #2039, .T. ) ;
#8936=CARTESIAN_POINT ( 'NONE',  ( -2.129528971937844517, -4.944374999999755715, -2.592863122870853410 ) ) ;
#8942=CARTESIAN_POINT ( 'NONE',  ( -1.414968154826750535, -0.4995676945082624387, 3.878355829113487641 ) ) ;
#8952=CARTESIAN_POINT ( 'NONE',  ( 1.869272562217232592, -3.171875000000011990, -3.494952631674145938 ) ) ;
#8957=ADVANCED_FACE ( 'NONE', ( #14474 ), #6436, .T. ) ;
#8963=CARTESIAN_POINT ( 'NONE',  ( 1.555132164185506927, 2.118440305037800009, 4.500000000000001776 ) ) ;
#8972=CARTESIAN_POINT ( 'NONE',  ( 1.779210140229175563, -1.756874999999983755, -3.331607052712223016 ) ) ;
#8991=CARTESIAN_POINT ( 'NONE',  ( 2.769370807496521980, -0.7100000000000333822, -2.767918543042355850 ) ) ;
#8992=AXIS2_PLACEMENT_3D ( 'NONE', #6205, #8360, #6052 ) ;
#8997=CARTESIAN_POINT ( 'NONE',  ( 3.738955316585249822, -1.078124999999896527, -2.000248979885406619 ) ) ;
#8999=CONICAL_SURFACE ( 'NONE', #10988, 3.250000000000015987, 0.4363323129985828275 ) ;
#9017=DIRECTION ( 'NONE',  ( 0.000000000000000000, -0.000000000000000000, -1.000000000000000000 ) ) ;
#9019=CARTESIAN_POINT ( 'NONE',  ( 2.619799856955864925, -4.694374999999869402, -2.148899555557211904 ) ) ;
#9029=CARTESIAN_POINT ( 'NONE',  ( 4.164680137118252468, -1.031249999999941602, -0.8299691317567963189 ) ) ;
#9044=VECTOR ( 'NONE', #10306, 1000.000000000000000 ) ;
#9045=CARTESIAN_POINT ( 'NONE',  ( 2.864761595209854406, -5.109375000000294875, -2.352813015294751953 ) ) ;
#9058=ORIENTED_EDGE ( 'NONE', *, *, #1858, .F. ) ;
#9064=CARTESIAN_POINT ( 'NONE',  ( -2.834780744084784754, -6.006874999999924469, -1.516137112471814818 ) ) ;
#9068=VERTEX_POINT ( 'NONE', #11445 ) ;
#9070=CARTESIAN_POINT ( 'NONE',  ( 1.382436512939505757, -5.811713562372810671, 3.339933979889968541 ) ) ;
#9071=CARTESIAN_POINT ( 'NONE',  ( -3.204583014436136690, -1.178749999999988640, 2.140022251743640691 ) ) ;
#9073=CARTESIAN_POINT ( 'NONE',  ( -3.121978066431621901, -2.609375000000007550, 2.560763078121147451 ) ) ;
#9076=CARTESIAN_POINT ( 'NONE',  ( 4.119136937081602667, 2.375954066961626143, 1.865445541641002514 ) ) ;
#9077=CARTESIAN_POINT ( 'NONE',  ( -2.641694630006354405, -1.640624999999979572, 3.221290409975102520 ) ) ;
#9088=CARTESIAN_POINT ( 'NONE',  ( -2.211816241884709822, -3.944375000000018172, -2.696513105594267046 ) ) ;
#9090=CARTESIAN_POINT ( 'NONE',  ( 5.196152422706631135, 0.1227504548087541975, -1.122964458370237425E-15 ) ) ;
#9094=CARTESIAN_POINT ( 'NONE',  ( -0.9842438906765387241, -0.4995676945082616061, 3.993364550929547896 ) ) ;
#9101=VERTEX_POINT ( 'NONE', #7810 ) ;
#9102=CARTESIAN_POINT ( 'NONE',  ( -3.490494984142799684, -1.406250000000081268, -2.330449509171077516 ) ) ;
#9104=CARTESIAN_POINT ( 'NONE',  ( -3.042761669814863623, -3.389838562372958997, -2.495273549889642783 ) ) ;
#9105=DIRECTION ( 'NONE',  ( -1.000000000000000000, -1.682335022489801357E-15, 0.000000000000000000 ) ) ;
#9108=APPLICATION_CONTEXT ( 'automotive_design' ) ;
#9117=CARTESIAN_POINT ( 'NONE',  ( -3.976927128516821952, -0.1006259897310525647, 0.3906606232675428059 ) ) ;
#9119=CARTESIAN_POINT ( 'NONE',  ( 3.341236413112389947, -1.663124999999897824, -1.787503410618120459 ) ) ;
#9120=CARTESIAN_POINT ( 'NONE',  ( -2.598076211353316012, 0.1227504548087343245, -4.499999999999999112 ) ) ;
#9125=CARTESIAN_POINT ( 'NONE',  ( 3.980852709490799501, -0.4995676945082488940, -0.4039315514682934039 ) ) ;
#9138=CARTESIAN_POINT ( 'NONE',  ( -1.970263329862414148, -6.342963562372986530, -2.946344977785408936 ) ) ;
#9139=CARTESIAN_POINT ( 'NONE',  ( -1.470831194960214861, -1.272500000000085230, 3.548278161707651090 ) ) ;
#9141=DIRECTION ( 'NONE',  ( 1.000000000000000000, 2.551930889570660354E-15, 0.000000000000000000 ) ) ;
#9142=CARTESIAN_POINT ( 'NONE',  ( 4.043635966909349122, -1.968749999999958034, 0.8028061105223156524 ) ) ;
#9147=CARTESIAN_POINT ( 'NONE',  ( 5.196152422706626695, 1.678847577293385296, -1.115338501812287204E-15 ) ) ;
#9157=ORIENTED_EDGE ( 'NONE', *, *, #1992, .F. ) ;
#9160=DIRECTION ( 'NONE',  ( 2.551930889570660354E-15, -1.000000000000000000, 0.000000000000000000 ) ) ;
#9161=CARTESIAN_POINT ( 'NONE',  ( 3.464101615137754386, 8.643436132524853256E-15, 2.999999999999999112 ) ) ;
#9162=DIRECTION ( 'NONE',  ( -1.000000000000000000, -2.505711687522054122E-15, 0.000000000000000000 ) ) ;
#9164=DIRECTION ( 'NONE',  ( -9.422394424380278809E-16, 1.000000000000000000, -0.000000000000000000 ) ) ;
#9165=CARTESIAN_POINT ( 'NONE',  ( -3.667454075173111505, -0.4995676945082688225, 2.138331822535261217 ) ) ;
#9172=CARTESIAN_POINT ( 'NONE',  ( 3.757405615841324042, -0.9218749999999823475, 2.009662442622283773 ) ) ;
#9174=CARTESIAN_POINT ( 'NONE',  ( -3.143458222507559352, -2.389838562372920805, -2.581159584719012745 ) ) ;
#9180=CARTESIAN_POINT ( 'NONE',  ( 1.274862231047225439E-15, -0.4995676945082591081, 0.000000000000000000 ) ) ;
#9187=CARTESIAN_POINT ( 'NONE',  ( 1.843713500184434917, -0.7568749999999383471, -3.447171040406491027 ) ) ;
#9190=CARTESIAN_POINT ( 'NONE',  ( 3.515159614179530045, -2.538124999999942677, 1.067305873498098912 ) ) ;
#9193=CARTESIAN_POINT ( 'NONE',  ( -1.673688575075004152E-15, 4.650702586819541295, 0.000000000000000000 ) ) ;
#9202=TOROIDAL_SURFACE ( 'NONE', #11695, 2.931404194366992400, 0.5000000000000000000 ) ;
#9204=CARTESIAN_POINT ( 'NONE',  ( 3.384491019838402170, -4.600625000000129639, -0.3324735777645302370 ) ) ;
#9207=B_SPLINE_CURVE_WITH_KNOTS ( 'NONE', 3,
 ( #664, #5417, #12544, #4238 ),
 .UNSPECIFIED., .F., .F.,
 ( 4, 4 ),
 ( 2.309401076754191683E-07, 0.002598307151460994141 ),
 .UNSPECIFIED. ) ;
#9212=CARTESIAN_POINT ( 'NONE',  ( -0.3809421545647762031, -0.8506249999999871969, -3.878187885777538035 ) ) ;
#9214=CARTESIAN_POINT ( 'NONE',  ( 0.8105829119240891556, -1.781250000000002887, 4.067378511145360420 ) ) ;
#9219=CARTESIAN_POINT ( 'NONE',  ( 1.951563910473907981E-15, 7.362500000000000711, 0.000000000000000000 ) ) ;
#9223=ORIENTED_EDGE ( 'NONE', *, *, #194, .F. ) ;
#9227=ORIENTED_EDGE ( 'NONE', *, *, #1373, .F. ) ;
#9234=CARTESIAN_POINT ( 'NONE',  ( -2.465526969817838587, -3.960000000000052811, -2.463696919996925416 ) ) ;
#9236=FACE_OUTER_BOUND ( 'NONE', #13583, .T. ) ;
#9238=AXIS2_PLACEMENT_3D ( 'NONE', #12359, #10017, #12428 ) ;
#9253=CARTESIAN_POINT ( 'NONE',  ( 4.232448940998905229, -0.9843749999998714362, 0.4153177470904050317 ) ) ;
#9256=CARTESIAN_POINT ( 'NONE',  ( -2.558190236227187331, -2.639838562373072239, 3.119474918453590373 ) ) ;
#9260=CARTESIAN_POINT ( 'NONE',  ( 3.012508034349780761, 2.058119353682402952, -3.782183026296719763 ) ) ;
#9265=CARTESIAN_POINT ( 'NONE',  ( 3.155399193331007712, -5.123732279192288352, -1.903239753125236078 ) ) ;
#9266=DIRECTION ( 'NONE',  ( -0.4999999999999998890, 0.000000000000000000, 0.8660254037844387076 ) ) ;
#9269=CARTESIAN_POINT ( 'NONE',  ( 3.555702576009056148, -5.046874999999973355, -1.077603027457875395 ) ) ;
#9273=CARTESIAN_POINT ( 'NONE',  ( 3.039561480324906029, -2.678749999999966214, -2.029833227700108544 ) ) ;
#9288=CARTESIAN_POINT ( 'NONE',  ( 2.417253850353039191, -4.460000000000003517, 2.418486108946755753 ) ) ;
#9290=ORIENTED_EDGE ( 'NONE', *, *, #10959, .T. ) ;
#9292=CARTESIAN_POINT ( 'NONE',  ( 3.706442405453559630, -4.983588562372924358, 0.3636771760149511423 ) ) ;
#9298=CARTESIAN_POINT ( 'NONE',  ( -4.130341191321600824, 2.356280171323974937, 1.846039204036427961 ) ) ;
#9299=CARTESIAN_POINT ( 'NONE',  ( 4.781720599710156172, 2.058119353682408725, 0.7178169737032801256 ) ) ;
#9304=CARTESIAN_POINT ( 'NONE',  ( 0.6569748927284305706, -4.803749999999888054, -3.309289439050846937 ) ) ;
#9310=ORIENTED_EDGE ( 'NONE', *, *, #5174, .F. ) ;
#9311=VERTEX_POINT ( 'NONE', #8796 ) ;
#9314=CIRCLE ( 'NONE', #3379, 4.296275033669348709 ) ;
#9324=DIRECTION ( 'NONE',  ( -2.551930889570659960E-15, 1.000000000000000000, 0.000000000000000000 ) ) ;
#9331=EDGE_LOOP ( 'NONE', ( #7746, #12342, #9223 ) ) ;
#9333=CARTESIAN_POINT ( 'NONE',  ( -3.873284713637146215, -1.437499999999919620, -1.605572741981209139 ) ) ;
#9336=CARTESIAN_POINT ( 'NONE',  ( -3.358725955652476891, -2.592963562373010955, 2.245994589438188971 ) ) ;
#9350=CARTESIAN_POINT ( 'NONE',  ( -3.589096097608166058, -5.468749999999688249, -0.7148808183696577778 ) ) ;
#9353=CARTESIAN_POINT ( 'NONE',  ( 2.315514200798038047, -2.725624999999891607, -2.819975302942780537 ) ) ;
#9366=CARTESIAN_POINT ( 'NONE',  ( -2.189584623831577037, -4.225624999999936016, 2.666627758504862111 ) ) ;
#9370=CARTESIAN_POINT ( 'NONE',  ( -2.414341998011519497, -4.358588562372940345, -2.943449326273882338 ) ) ;
#9375=PLANE ( 'NONE',  #7861 ) ;
#9380=CARTESIAN_POINT ( 'NONE',  ( 0.6449049195797605938, -5.366250000000259313, 3.235821967343390337 ) ) ;
#9382=VERTEX_POINT ( 'NONE', #5167 ) ;
#9386=VERTEX_POINT ( 'NONE', #10899 ) ;
#9388=CARTESIAN_POINT ( 'NONE',  ( -0.3421672931279376995, -3.850625000000083009, -3.483230393025887661 ) ) ;
#9392=CARTESIAN_POINT ( 'NONE',  ( -2.193587568844167279, 1.881091898548003183, -4.499999999999998224 ) ) ;
#9403=CARTESIAN_POINT ( 'NONE',  ( 2.056459069434533049, -0.1718749999999378830, -3.844889943890866579 ) ) ;
#9405=CARTESIAN_POINT ( 'NONE',  ( -2.854913087873755195, -2.624213562373173048, 2.853407187448114612 ) ) ;
#9417=CARTESIAN_POINT ( 'NONE',  ( 3.407468303614469285, -3.921874999999769074, 1.822475935421856708 ) ) ;
#9420=EDGE_CURVE ( 'NONE', #4633, #5514, #4998, .T. ) ;
#9421=CARTESIAN_POINT ( 'NONE',  ( -3.456628223078394679, -2.022499999999918252, -1.432834870345867984 ) ) ;
#9425=EDGE_CURVE ( 'NONE', #1386, #4034, #12875, .T. ) ;
#9428=DIRECTION ( 'NONE',  ( -2.551930889570658776E-15, 1.000000000000000000, 0.000000000000000000 ) ) ;
#9437=CARTESIAN_POINT ( 'NONE',  ( -1.647113530155737360, -3.913124999999971099, -3.078783428963379531 ) ) ;
#9441=CARTESIAN_POINT ( 'NONE',  ( 3.215963366055881512, -3.905463562372929243, 2.147137851111217799 ) ) ;
#9445=CIRCLE ( 'NONE', #4757, 4.362044368365340041 ) ;
#9450=CARTESIAN_POINT ( 'NONE',  ( -2.465526969817838587, -3.960000000000052811, -2.463696919996925416 ) ) ;
#9454=CARTESIAN_POINT ( 'NONE',  ( -1.629699455448989389E-14, 8.699999999999999289, 5.655858585055787181E-29 ) ) ;
#9458=EDGE_LOOP ( 'NONE', ( #5799, #4259, #10319, #8762, #323 ) ) ;
#9461=CARTESIAN_POINT ( 'NONE',  ( -3.335258087793214088, -3.022499999999893827, -1.380066378191329379 ) ) ;
#9464=CARTESIAN_POINT ( 'NONE',  ( -2.598076211353319565, 1.678847577293365978, -4.499999999999999112 ) ) ;
#9473=CARTESIAN_POINT ( 'NONE',  ( -3.250000000000014211, 7.362499999999993605, 3.980102097228917460E-16 ) ) ;
#9481=CARTESIAN_POINT ( 'NONE',  ( -2.666008743340035902, -1.358588562373146624, -3.250302320816439217 ) ) ;
#9491=EDGE_CURVE ( 'NONE', #5205, #1380, #5238, .T. ) ;
#9497=CARTESIAN_POINT ( 'NONE',  ( -0.7342670381812395064, -4.718750000000252243, 3.686397723581088304 ) ) ;
#9499=CARTESIAN_POINT ( 'NONE',  ( -3.419120714393278249, -1.006874999999977760, -1.825951887684714503 ) ) ;
#9501=TOROIDAL_SURFACE ( 'NONE', #1343, -1.151041666666720031, 4.401041666666736241 ) ;
#9515=CARTESIAN_POINT ( 'NONE',  ( 3.503842902704710660, -2.631874999999911147, -1.061889326425361268 ) ) ;
#9516=EDGE_LOOP ( 'NONE', ( #9936, #10792, #5009, #11626, #1028, #6546, #14498 ) ) ;
#9523=CARTESIAN_POINT ( 'NONE',  ( -2.598076211353315124, -6.630110937211234507E-15, 4.500000000000000888 ) ) ;
#9527=CARTESIAN_POINT ( 'NONE',  ( 0.6686498792469546260, -4.366249999999815223, 3.366016213005436075 ) ) ;
#9532=FACE_OUTER_BOUND ( 'NONE', #9331, .T. ) ;
#9536=AXIS2_PLACEMENT_3D ( 'NONE', #3997, #8727, #2839 ) ;
#9538=CARTESIAN_POINT ( 'NONE',  ( -2.795825449145424191, -2.975624999999864517, -2.292747793747622609 ) ) ;
#9555=ORIENTED_EDGE ( 'NONE', *, *, #11251, .F. ) ;
#9559=CARTESIAN_POINT ( 'NONE',  ( -4.185213075431162721, -1.499213562373157949, -0.001111502682336006596 ) ) ;
#9561=TOROIDAL_SURFACE ( 'NONE', #4134, 2.093999815491831562, 0.2500000000000000000 ) ;
#9565=PRODUCT ( 'Self-Tapping Grease Fitting_8742T12', 'Self-Tapping Grease Fitting_8742T12', '', ( #5652 ) ) ;
#9573=CARTESIAN_POINT ( 'NONE',  ( 3.775473633219732505, -4.031249999999629630, -0.7524242524445519109 ) ) ;
#9587=DIRECTION ( 'NONE',  ( 6.982962677686266711E-15, 6.579622859988665673E-30, 1.000000000000000000 ) ) ;
#9589=AXIS2_PLACEMENT_3D ( 'NONE', #5701, #9164, #4595 ) ;
#9591=CARTESIAN_POINT ( 'NONE',  ( 3.535094671665901078, -3.584999999999991083, -0.001309597400350227814 ) ) ;
#9599=CARTESIAN_POINT ( 'NONE',  ( -3.897114317029972685, -9.945166405816852549E-15, -2.249999999999999112 ) ) ;
#9605=CARTESIAN_POINT ( 'NONE',  ( 0.6849063648203621568, -3.803749999999915143, -3.438650935610223947 ) ) ;
#9612=EDGE_LOOP ( 'NONE', ( #5677, #3434, #9937, #8171, #9227 ) ) ;
#9636=CARTESIAN_POINT ( 'NONE',  ( -0.4250114624646683659, -0.2656249999999867883, -4.327074173745135255 ) ) ;
#9637=CARTESIAN_POINT ( 'NONE',  ( 0.8248545445007013921, -1.217963562373110653, -4.141066646055018730 ) ) ;
#9641=B_SPLINE_CURVE_WITH_KNOTS ( 'NONE', 3,
 ( #12589, #5302, #12513, #6630 ),
 .UNSPECIFIED., .F., .F.,
 ( 4, 4 ),
 ( 0.002598307151460994141, 0.005196383362814307842 ),
 .UNSPECIFIED. ) ;
#9648=CARTESIAN_POINT ( 'NONE',  ( -3.613419487966115895, -3.562500000000009326, 1.498272701152596031 ) ) ;
#9650=CARTESIAN_POINT ( 'NONE',  ( -0.3809421545647762031, -0.8506249999999871969, -3.878187885777538035 ) ) ;
#9656=DIRECTION ( 'NONE',  ( -2.551930889570659960E-15, 1.000000000000000000, 0.000000000000000000 ) ) ;
#9663=CARTESIAN_POINT ( 'NONE',  ( -0.3421672931279376995, -3.850625000000083009, -3.483230393025888105 ) ) ;
#9676=CARTESIAN_POINT ( 'NONE',  ( -2.894177851434075244, -3.991249999999941789, -1.934899151906914305 ) ) ;
#9688=CARTESIAN_POINT ( 'NONE',  ( -1.038475776471825762, -3.288125000000012843, 3.420226703972062854 ) ) ;
#9692=CARTESIAN_POINT ( 'NONE',  ( -1.629699455448989389E-14, 8.699999999999999289, 5.655858585055787181E-29 ) ) ;
#9707=CARTESIAN_POINT ( 'NONE',  ( -2.933994605034233150, -5.163125000000027498, 1.567297863280187054 ) ) ;
#9709=CARTESIAN_POINT ( 'NONE',  ( -4.359283389060221836, 0.4687500000000111022, 0.8687415714326495175 ) ) ;
#9710=CARTESIAN_POINT ( 'NONE',  ( -3.999387421850409741, -1.546088562373119979, 1.212041425752152568 ) ) ;
#9715=CONICAL_SURFACE ( 'NONE', #5777, 4.500000000000000888, 0.7853981633974500554 ) ;
#9724=EDGE_CURVE ( 'NONE', #160, #2409, #13913, .T. ) ;
#9728=CARTESIAN_POINT ( 'NONE',  ( 3.389018004338130385, -4.078125000000095035, -1.813062472674689340 ) ) ;
#9730=CARTESIAN_POINT ( 'NONE',  ( 3.568345045357413703, -3.936713562373220565, 1.479150544514123089 ) ) ;
#9732=CARTESIAN_POINT ( 'NONE',  ( 2.697785604507370483, -1.459999999999946008, 2.699193867783821865 ) ) ;
#9739=CARTESIAN_POINT ( 'NONE',  ( 3.138279930143428764, -5.305558064392307038, 1.406575084002399612 ) ) ;
#9742=CIRCLE ( 'NONE', #13472, 0.8000000000000113687 ) ;
#9743=ORIENTED_EDGE ( 'NONE', *, *, #8874, .T. ) ;
#9747=CARTESIAN_POINT ( 'NONE',  ( 2.950365215318708323, -3.491249999999835651, 1.969791294043586660 ) ) ;
#9767=CARTESIAN_POINT ( 'NONE',  ( 2.674095735623811088, -1.709999999999972209, -2.676057788957662886 ) ) ;
#9770=CARTESIAN_POINT ( 'NONE',  ( 2.736090332400194836, -3.875000000000003553, 2.737522629006357455 ) ) ;
#9787=CARTESIAN_POINT ( 'NONE',  ( 2.063655046872799659, -5.725624999999673115, -2.513280214060439999 ) ) ;
#9790=CARTESIAN_POINT ( 'NONE',  ( -1.287538504858034338, -4.897500000000167830, -3.105113058795574421 ) ) ;
#9806=SPHERICAL_SURFACE ( 'NONE', #11296, 0.8600000000000014300 ) ;
#9807=CARTESIAN_POINT ( 'NONE',  ( -1.185531852251327400, -2.296875000000050182, -3.903075577084617720 ) ) ;
#9811=CARTESIAN_POINT ( 'NONE',  ( 0.0009559351216548812522, -5.249213562373182818, -3.689142743541748093 ) ) ;
#9821=CARTESIAN_POINT ( 'NONE',  ( 2.621470655598105548, -5.354113571045281184, 2.112355036808595710 ) ) ;
#9828=CARTESIAN_POINT ( 'NONE',  ( 9.531855622864829864E-16, 8.384405323238834029, 0.000000000000000000 ) ) ;
#9829=CARTESIAN_POINT ( 'NONE',  ( 2.743301530724825188, -3.475625000000028386, 2.252549412313518573 ) ) ;
#9841=ORIENTED_EDGE ( 'NONE', *, *, #2304, .F. ) ;
#9850=CARTESIAN_POINT ( 'NONE',  ( 3.341236413112389947, -1.663124999999897824, -1.787503410618120459 ) ) ;
#9852=CARTESIAN_POINT ( 'NONE',  ( -3.745604523531179897, -3.546874999999923173, 1.135144126415479793 ) ) ;
#9854=DIRECTION ( 'NONE',  ( 6.982962677686266711E-15, 6.579622859988665673E-30, 1.000000000000000000 ) ) ;
#9866=CARTESIAN_POINT ( 'NONE',  ( 2.894038744318182310, -5.506874999999972431, 1.545501402921559908 ) ) ;
#9869=CARTESIAN_POINT ( 'NONE',  ( -3.322613055092911161, -5.069375000000116316, -0.3280989749989032256 ) ) ;
#9883=CARTESIAN_POINT ( 'NONE',  ( 3.935506471057187206, -2.046874999999910738, -1.192685225358429912 ) ) ;
#9902=CARTESIAN_POINT ( 'NONE',  ( -2.135074830120813782, -1.241249999999904707, 3.197897516496418735 ) ) ;
#9907=CARTESIAN_POINT ( 'NONE',  ( 1.787440017715160590, -5.131417235833041879, -3.208234933698080660 ) ) ;
#9909=DIRECTION ( 'NONE',  ( -2.551930889570659960E-15, 1.000000000000000000, 0.000000000000000000 ) ) ;
#9922=CARTESIAN_POINT ( 'NONE',  ( 3.601230736643932673, -2.553749999999958220, 0.7149504581460995878 ) ) ;
#9924=CARTESIAN_POINT ( 'NONE',  ( -3.249648180954406662, -3.593749999999990230, 2.170113394669044293 ) ) ;
#9930=DIRECTION ( 'NONE',  ( -1.000000000000000000, -2.548822376660340629E-15, 0.000000000000000000 ) ) ;
#9936=ORIENTED_EDGE ( 'NONE', *, *, #13797, .T. ) ;
#9937=ORIENTED_EDGE ( 'NONE', *, *, #10743, .T. ) ;
#9939=CARTESIAN_POINT ( 'NONE',  ( -2.129528971937844961, -4.944374999999755715, -2.592863122870769921 ) ) ;
#9945=CIRCLE ( 'NONE', #4754, 0.8600000000000014300 ) ;
#9955=SURFACE_STYLE_FILL_AREA ( #14610 ) ;
#9956=CARTESIAN_POINT ( 'NONE',  ( 3.796719365261179480, -2.062499999999996003, -1.574265350336458313 ) ) ;
#9959=CARTESIAN_POINT ( 'NONE',  ( 1.485839477460144442, -3.811713562373131303, 3.583429635616939724 ) ) ;
#9960=DIRECTION ( 'NONE',  ( -1.224646799147353207E-16, -1.153910517212117582E-31, 1.000000000000000000 ) ) ;
#9969=DIRECTION ( 'NONE',  ( 1.747085166004344019E-15, -1.000000000000000000, 0.000000000000000000 ) ) ;
#9970=VECTOR ( 'NONE', #13040, 1000.000000000000000 ) ;
#9976=CARTESIAN_POINT ( 'NONE',  ( -3.563362751979611165, -1.147500000000009734, 1.477520127916053694 ) ) ;
#9981=CARTESIAN_POINT ( 'NONE',  ( -1.438230851946688649, -5.195093061962212211, -3.273449327035441669 ) ) ;
#10000=CARTESIAN_POINT ( 'NONE',  ( -3.733522804429754149, -2.085000000000140741, 0.001371824453762974898 ) ) ;
#10002=CARTESIAN_POINT ( 'NONE',  ( -2.475833455637627800, -3.640624999999937383, 3.015200003105952042 ) ) ;
#10008=ADVANCED_FACE ( 'NONE', ( #6558 ), #11275, .F. ) ;
#10010=CARTESIAN_POINT ( 'NONE',  ( -4.119136937081615990, 2.375954066961606159, -1.865445541641003624 ) ) ;
#10014=B_SPLINE_CURVE_WITH_KNOTS ( 'NONE', 3,
 ( #7092, #11814, #1179, #10638 ),
 .UNSPECIFIED., .F., .F.,
 ( 4, 4 ),
 ( 0.8333333174325897597, 0.8334051513705891256 ),
 .UNSPECIFIED. ) ;
#10017=DIRECTION ( 'NONE',  ( 1.224646799147353207E-16, 1.153910517212117582E-31, 1.000000000000000000 ) ) ;
#10023=CARTESIAN_POINT ( 'NONE',  ( -1.673688575075003955E-15, 4.650702586819541295, 0.000000000000000000 ) ) ;
#10024=CARTESIAN_POINT ( 'NONE',  ( -2.968563080203957316, -6.022500000000311715, -1.228311040920463393 ) ) ;
#10025=CARTESIAN_POINT ( 'NONE',  ( 1.375881166777175254E-16, 9.250000000000000000, 0.000000000000000000 ) ) ;
#10026=FACE_OUTER_BOUND ( 'NONE', #517, .T. ) ;
#10029=CARTESIAN_POINT ( 'NONE',  ( 0.3463240970199374935, -0.4995676945082583309, 4.051387190110659731 ) ) ;
#10030=CARTESIAN_POINT ( 'NONE',  ( 2.417253850352953481, -4.460000000000003517, 2.418486108946755309 ) ) ;
#10031=ORIENTED_EDGE ( 'NONE', *, *, #10413, .F. ) ;
#10034=ORIENTED_EDGE ( 'NONE', *, *, #993, .F. ) ;
#10036=CARTESIAN_POINT ( 'NONE',  ( -2.240749814637992721, -2.656250000000047073, 3.351605112894145311 ) ) ;
#10054=CARTESIAN_POINT ( 'NONE',  ( -3.419120714393279137, -1.006874999999977760, -1.825951887684667208 ) ) ;
#10061=DIRECTION ( 'NONE',  ( -9.422394424380278809E-16, 1.000000000000000000, -0.000000000000000000 ) ) ;
#10068=ADVANCED_FACE ( 'NONE', ( #10026 ), #9202, .F. ) ;
#10075=CARTESIAN_POINT ( 'NONE',  ( 3.175740969752042453, -5.921088562373065578, 1.695960816590878384 ) ) ;
#10077=CARTESIAN_POINT ( 'NONE',  ( 0.001419932108912198322, -3.750000000000078160, 3.886924930609184869 ) ) ;
#10081=CARTESIAN_POINT ( 'NONE',  ( -3.778928804394623864, 2.374507716408091884, -2.454703312603006893 ) ) ;
#10082=CARTESIAN_POINT ( 'NONE',  ( -3.681901511607714728, -1.578124999999909850, 1.966760930092153137 ) ) ;
#10085=DIRECTION ( 'NONE',  ( -9.422394424380278809E-16, 1.000000000000000000, -0.000000000000000000 ) ) ;
#10101=CARTESIAN_POINT ( 'NONE',  ( 2.200487690058695822, -0.4995676945082536680, 3.334363425755398680 ) ) ;
#10109=ORIENTED_EDGE ( 'NONE', *, *, #2013, .F. ) ;
#10110=CARTESIAN_POINT ( 'NONE',  ( 1.186295216973591859, -2.203125000000055067, -3.915803815994934656 ) ) ;
#10117=CARTESIAN_POINT ( 'NONE',  ( 2.396990258891838366, 1.779390553524114571, 4.499999999999998224 ) ) ;
#10124=CARTESIAN_POINT ( 'NONE',  ( -1.487946254897667187, -0.8975000000000187272, -3.594883137563858799 ) ) ;
#10129=FACE_OUTER_BOUND ( 'NONE', #11834, .T. ) ;
#10140=CARTESIAN_POINT ( 'NONE',  ( -2.332209567415143514, -5.358588562372849751, -2.839672270176649693 ) ) ;
#10141=CARTESIAN_POINT ( 'NONE',  ( -3.976927128516043908, -0.1006259897310523566, 0.3906606232675376988 ) ) ;
#10144=CARTESIAN_POINT ( 'NONE',  ( 2.541707380700019225, -2.859374999999939160, 3.094782911937220771 ) ) ;
#10149=CARTESIAN_POINT ( 'NONE',  ( 3.919974135967671636, -1.062500000000018652, -1.622483930095183213 ) ) ;
#10150=CARTESIAN_POINT ( 'NONE',  ( 3.372444421885775423, -0.4995676945082423992, 2.006840812041871924 ) ) ;
#10158=EDGE_LOOP ( 'NONE', ( #1514, #7208, #6749, #10490, #57 ) ) ;
#10166=CARTESIAN_POINT ( 'NONE',  ( 2.864129664102274209, -0.4995676945082523357, 2.739103314933886590 ) ) ;
#10168=ADVANCED_FACE ( 'NONE', ( #9236 ), #11418, .F. ) ;
#10170=CARTESIAN_POINT ( 'NONE',  ( 0.3227798623957477964, -5.350624999999817888, 3.285751646651179136 ) ) ;
#10177=AXIS2_PLACEMENT_3D ( 'NONE', #13539, #3048, #2904 ) ;
#10179=CARTESIAN_POINT ( 'NONE',  ( -2.385544021208493071, -0.6562499999999052980, 3.573005751195701407 ) ) ;
#10180=EDGE_LOOP ( 'NONE', ( #13089, #12941, #11986, #12113, #283 ) ) ;
#10181=CARTESIAN_POINT ( 'NONE',  ( -3.849161768156871499, -3.467963562373198805, -0.7666958849875432636 ) ) ;
#10187=EDGE_CURVE ( 'NONE', #11015, #6676, #5263, .T. ) ;
#10191=DIRECTION ( 'NONE',  ( 1.000000000000000000, 0.000000000000000000, 1.224646799147353454E-16 ) ) ;
#10196=EDGE_LOOP ( 'NONE', ( #8933, #12299, #12902 ) ) ;
#10198=CARTESIAN_POINT ( 'NONE',  ( -3.456628223078487050, -2.022499999999918252, -1.432834870345867984 ) ) ;
#10199=ORIENTED_EDGE ( 'NONE', *, *, #12447, .F. ) ;
#10213=CARTESIAN_POINT ( 'NONE',  ( -2.785343681203864552, -4.991249999999938680, -1.859602269982786105 ) ) ;
#10219=CARTESIAN_POINT ( 'NONE',  ( 2.994712326477856568, -5.905463562373213904, 2.002119754258344653 ) ) ;
#10220=CARTESIAN_POINT ( 'NONE',  ( -3.419120714393278249, -1.006874999999977760, -1.825951887684714503 ) ) ;
#10223=CARTESIAN_POINT ( 'NONE',  ( -0.7834809220335302582, -2.718750000000123013, 3.946322201046845279 ) ) ;
#10227=CARTESIAN_POINT ( 'NONE',  ( -2.385544021208493071, -0.6562499999999052980, 3.573005751195701407 ) ) ;
#10238=EDGE_CURVE ( 'NONE', #1688, #7901, #5768, .T. ) ;
#10241=CARTESIAN_POINT ( 'NONE',  ( -1.336190917661197242, -3.897499999999990195, -3.228188129988408317 ) ) ;
#10253=CIRCLE ( 'NONE', #12251, 0.8000000000000113687 ) ;
#10260=CARTESIAN_POINT ( 'NONE',  ( -3.681901511607714728, -1.578124999999909850, 1.966760930092153137 ) ) ;
#10262=CARTESIAN_POINT ( 'NONE',  ( 3.813698945254171413, -1.936713562373129083, 1.578067310789440958 ) ) ;
#10270=FACE_OUTER_BOUND ( 'NONE', #2850, .T. ) ;
#10275=CARTESIAN_POINT ( 'NONE',  ( 2.195116763761142842, -0.4287499999998638511, 3.287093781494352829 ) ) ;
#10280=CARTESIAN_POINT ( 'NONE',  ( 3.059130242547580814, -2.491250000000117204, 2.045191655759024396 ) ) ;
#10288=CARTESIAN_POINT ( 'NONE',  ( 3.519978383818244350, -5.234011689638929710, 0.1468655065803234350 ) ) ;
#10293=LINE ( 'NONE', #12786, #4300 ) ;
#10297=CARTESIAN_POINT ( 'NONE',  ( 1.879752899984456604, -4.741249999999911147, -2.811701655874746741 ) ) ;
#10303=CARTESIAN_POINT ( 'NONE',  ( -3.028821173363755115, -5.592963562372932351, 2.025409581771773659 ) ) ;
#10305=CARTESIAN_POINT ( 'NONE',  ( -1.872693635133505063, -0.2568750000000157852, 3.506634376076539716 ) ) ;
#10306=DIRECTION ( 'NONE',  ( 2.551930889570659960E-15, -1.000000000000000000, -0.000000000000000000 ) ) ;
#10307=CARTESIAN_POINT ( 'NONE',  ( 2.601763032574845536, -2.140624999999891198, -3.168547547573197232 ) ) ;
#10311=CARTESIAN_POINT ( 'NONE',  ( 3.298003658611986744, -0.8906249999999793499, 2.704611316345772121 ) ) ;
#10317=ORIENTED_EDGE ( 'NONE', *, *, #13673, .T. ) ;
#10319=ORIENTED_EDGE ( 'NONE', *, *, #2039, .F. ) ;
#10333=DIRECTION ( 'NONE',  ( 1.000000000000000000, 2.551930889570659960E-15, 0.000000000000000000 ) ) ;
#10340=CARTESIAN_POINT ( 'NONE',  ( -4.136606882479101799, -0.4531250000000215938, -1.256032681398332906 ) ) ;
#10342=CARTESIAN_POINT ( 'NONE',  ( -1.857982519382167963, -3.327338562373031383, -3.478237815464837901 ) ) ;
#10350=DIRECTION ( 'NONE',  ( -0.7933533402912378296, 0.6087614290087172142, 0.000000000000000000 ) ) ;
#10355=CARTESIAN_POINT ( 'NONE',  ( -2.043454634528946823, -5.343749999999893419, -3.055809177479244632 ) ) ;
#10357=CARTESIAN_POINT ( 'NONE',  ( 3.380062874710183074, -2.647499999999996856, -1.401527478686670491 ) ) ;
#10364=EDGE_CURVE ( 'NONE', #8567, #6676, #3663, .T. ) ;
#10366=EDGE_CURVE ( 'NONE', #6229, #8371, #1736, .T. ) ;
#10371=CARTESIAN_POINT ( 'NONE',  ( 0.0008557816480051286256, -4.835000000000089670, -3.369777484087370656 ) ) ;
#10375=CARTESIAN_POINT ( 'NONE',  ( 1.365161570743866015, -6.186713562372902153, -3.293395229433107030 ) ) ;
#10376=EDGE_CURVE ( 'NONE', #10851, #7901, #2526, .T. ) ;
#10377=CARTESIAN_POINT ( 'NONE',  ( 0.3809421545653356445, -0.8193749999999933031, -3.882302026224086156 ) ) ;
#10379=CARTESIAN_POINT ( 'NONE',  ( -3.736626632189893105, -2.562500000000080824, 1.546606261444747554 ) ) ;
#10382=FACE_BOUND ( 'NONE', #14440, .T. ) ;
#10394=CARTESIAN_POINT ( 'NONE',  ( 2.642398951855386535, -4.475625000000026610, 2.166914421091147069 ) ) ;
#10397=CARTESIAN_POINT ( 'NONE',  ( 2.396990258880748570, 1.779390553529661467, -4.500000000000000000 ) ) ;
#10409=CARTESIAN_POINT ( 'NONE',  ( 3.935370341889717682, -0.9375000000000351941, 1.628420556316443557 ) ) ;
#10411=CARTESIAN_POINT ( 'NONE',  ( 1.517146869108012996, -3.186713562373090447, -3.659994983997363782 ) ) ;
#10413=EDGE_CURVE ( 'NONE', #13125, #1380, #293, .T. ) ;
#10416=CARTESIAN_POINT ( 'NONE',  ( 3.675091696978328493, 2.375954066961625255, -2.634554458358995710 ) ) ;
#10426=CARTESIAN_POINT ( 'NONE',  ( -0.3809421545647762586, -0.8506249999999871969, -3.878187885777443444 ) ) ;
#10429=CARTESIAN_POINT ( 'NONE',  ( -1.750120246539625946, -2.256875000000012843, 3.272202384321437840 ) ) ;
#10430=ADVANCED_FACE ( 'NONE', ( #10457 ), #12944, .T. ) ;
#10438=VERTEX_POINT ( 'NONE', #8065 ) ;
#10443=CARTESIAN_POINT ( 'NONE',  ( -1.864549691619356464, -4.928749999999819664, -2.792029179168366682 ) ) ;
#10448=CARTESIAN_POINT ( 'NONE',  ( 2.643008371794767886, -4.874213562373096664, 2.644382268777536016 ) ) ;
#10450=CARTESIAN_POINT ( 'NONE',  ( 3.280408283555247717, -0.4912499999999521139, 2.190169342145847242 ) ) ;
#10452=CARTESIAN_POINT ( 'NONE',  ( -0.001059456894846966344, -2.749999999999859224, 4.019249942169077272 ) ) ;
#10457=FACE_OUTER_BOUND ( 'NONE', #1301, .T. ) ;
#10460=CARTESIAN_POINT ( 'NONE',  ( -0.6461339251375918247, -5.303750000000252207, 3.244047683681893446 ) ) ;
#10490=ORIENTED_EDGE ( 'NONE', *, *, #1287, .F. ) ;
#10493=CARTESIAN_POINT ( 'NONE',  ( 1.953452353076893244, -1.828124999999917399, 3.651470988527475647 ) ) ;
#10495=CARTESIAN_POINT ( 'NONE',  ( 2.277851013824919058, -2.155463562373088671, -3.407093304313265847 ) ) ;
#10507=CARTESIAN_POINT ( 'NONE',  ( 3.701456747302541928, -5.015624999999988454, -0.3659357139933352987 ) ) ;
#10509=CIRCLE ( 'NONE', #845, 0.8600000000000014300 ) ;
#10510=CIRCLE ( 'NONE', #1351, 2.514916625122320948 ) ;
#10511=CARTESIAN_POINT ( 'NONE',  ( -2.896649075160178111, -1.975624999999826548, -2.378478989283399514 ) ) ;
#10526=CARTESIAN_POINT ( 'NONE',  ( -3.450064735799972748, -4.100625000000076348, 0.3410961574374388183 ) ) ;
#10527=EDGE_LOOP ( 'NONE', ( #2447, #9841, #8435, #6211 ) ) ;
#10530=CARTESIAN_POINT ( 'NONE',  ( -1.409846828270459262, -5.311713562373262754, -3.400129758324495377 ) ) ;
#10535=PLANE ( 'NONE',  #2393 ) ;
#10543=CARTESIAN_POINT ( 'NONE',  ( -2.763334307196396722, -5.178749999999838316, 1.847896475581856324 ) ) ;
#10553=CARTESIAN_POINT ( 'NONE',  ( -3.535952561574606801, -3.053750000000104770, -0.7042925846621640451 ) ) ;
#10557=CARTESIAN_POINT ( 'NONE',  ( 2.644209610478730266, -4.874999999999846345, 2.642267524923772370 ) ) ;
#10577=CARTESIAN_POINT ( 'NONE',  ( 0.3887688439250656658, -3.233588562373015396, -3.936630488393996430 ) ) ;
#10592=CARTESIAN_POINT ( 'NONE',  ( -0.001042462806621457638, -0.3350000000001150946, 3.965061882346497590 ) ) ;
#10595=CARTESIAN_POINT ( 'NONE',  ( -0.7236788045118704993, -2.303749999999964437, 3.633254187536902435 ) ) ;
#10597=CARTESIAN_POINT ( 'NONE',  ( 1.403561989263864891E-14, -5.500000000000007994, 0.000000000000000000 ) ) ;
#10599=CARTESIAN_POINT ( 'NONE',  ( 1.403561989263863629E-14, -5.500000000000003553, 0.000000000000000000 ) ) ;
#10603=CARTESIAN_POINT ( 'NONE',  ( 1.951563910473907981E-15, 7.362500000000000711, 0.000000000000000000 ) ) ;
#10607=CARTESIAN_POINT ( 'NONE',  ( 3.341349309646173715, -4.553750000000432507, 0.6655201449779076794 ) ) ;
#10609=ORIENTED_EDGE ( 'NONE', *, *, #1091, .T. ) ;
#10611=CARTESIAN_POINT ( 'NONE',  ( 1.073618264594249583, -5.202338562372997188, -3.535945309138720738 ) ) ;
#10620=DIRECTION ( 'NONE',  ( -1.000000000000000000, -9.422394424380278809E-16, 0.000000000000000000 ) ) ;
#10622=CARTESIAN_POINT ( 'NONE',  ( 2.229831107420913838, -3.725624999999957776, -2.719112200499452126 ) ) ;
#10630=CARTESIAN_POINT ( 'NONE',  ( 2.822884439542639790, -2.694375000000075460, -2.318423337397389261 ) ) ;
#10632=CARTESIAN_POINT ( 'NONE',  ( 3.555702576009056148, -5.046874999999973355, -1.077603027457875395 ) ) ;
#10638=CARTESIAN_POINT ( 'NONE',  ( -4.296227084909979510, -0.4995677573761841406, -0.01166785054812304046 ) ) ;
#10641=CARTESIAN_POINT ( 'NONE',  ( 3.897114317029974462, 9.945166405816860437E-15, 2.249999999999999556 ) ) ;
#10647=CARTESIAN_POINT ( 'NONE',  ( -3.133198094827410518, 0.3749999999998852029, 3.135448188384045931 ) ) ;
#10650=CARTESIAN_POINT ( 'NONE',  ( -4.162815442996374848, -1.514838562373068909, 0.4115216691269514837 ) ) ;
#10656=VERTEX_POINT ( 'NONE', #6821 ) ;
#10662=CARTESIAN_POINT ( 'NONE',  ( -2.165165973034034685, -3.656250000000003997, 3.242962682996374912 ) ) ;
#10663=ORIENTED_EDGE ( 'NONE', *, *, #9724, .T. ) ;
#10667=CARTESIAN_POINT ( 'NONE',  ( 0.5890844654258655666, -5.395954183479145350, 3.259439424676229713 ) ) ;
#10677=DIRECTION ( 'NONE',  ( 1.000000000000000000, 0.000000000000000000, -6.982962677686266711E-15 ) ) ;
#10682=CARTESIAN_POINT ( 'NONE',  ( 3.273328345814468410, -3.522500000000126974, 1.356842221127620096 ) ) ;
#10687=CARTESIAN_POINT ( 'NONE',  ( 2.990110678052926296, -3.889838562373120645, 2.455230007768598011 ) ) ;
#10699=CARTESIAN_POINT ( 'NONE',  ( -3.450064735799886595, -4.100625000000076348, 0.3410961574374171690 ) ) ;
#10710=CARTESIAN_POINT ( 'NONE',  ( -3.184718056276182097, -3.006875000000130083, -1.703323619722481475 ) ) ;
#10713=CARTESIAN_POINT ( 'NONE',  ( 3.567009421182318896, -4.953124999999990230, 1.083052099369142818 ) ) ;
#10714=DIRECTION ( 'NONE',  ( -9.422394424380278809E-16, 1.000000000000000000, -0.000000000000000000 ) ) ;
#10718=CARTESIAN_POINT ( 'NONE',  ( 4.763139720814411504, 0.04639863247564436632, -0.7500000000000013323 ) ) ;
#10729=CARTESIAN_POINT ( 'NONE',  ( -9.797174393178998714E-17, 9.500000000000000000, 0.000000000000000000 ) ) ;
#10731=ORIENTED_EDGE ( 'NONE', *, *, #4000, .F. ) ;
#10733=CARTESIAN_POINT ( 'NONE',  ( 3.196188167093295895, -1.889838562373073350, 2.621106922562215669 ) ) ;
#10743=EDGE_CURVE ( 'NONE', #10656, #1386, #11713, .T. ) ;
#10750=CARTESIAN_POINT ( 'NONE',  ( 3.833377307806092649, -4.015625000000129674, -0.3765428855675501119 ) ) ;
#10752=CARTESIAN_POINT ( 'NONE',  ( -3.563362751979704868, -1.147500000000009734, 1.477520127916053472 ) ) ;
#10753=AXIS2_PLACEMENT_3D ( 'NONE', #14873, #10854, #15334 ) ;
#10755=CIRCLE ( 'NONE', #12001, 0.8600000000000014300 ) ;
#10756=CARTESIAN_POINT ( 'NONE',  ( -0.2942231418407759702, -5.377451219392755277, 3.333184271469537219 ) ) ;
#10773=CARTESIAN_POINT ( 'NONE',  ( 0.6849063648203621568, -3.803749999999915143, -3.438650935610224835 ) ) ;
#10785=EDGE_CURVE ( 'NONE', #8406, #7102, #10985, .T. ) ;
#10786=CARTESIAN_POINT ( 'NONE',  ( -3.166267757014364914, -3.163124999999988862, 1.693910156975028780 ) ) ;
#10792=ORIENTED_EDGE ( 'NONE', *, *, #8500, .T. ) ;
#10797=CARTESIAN_POINT ( 'NONE',  ( -3.166267757014364914, -3.163124999999988862, 1.693910156975028780 ) ) ;
#10798=FACE_BOUND ( 'NONE', #12835, .T. ) ;
#10800=DIRECTION ( 'NONE',  ( -1.000000000000000000, 0.000000000000000000, 0.000000000000000000 ) ) ;
#10807=CARTESIAN_POINT ( 'NONE',  ( -1.006616814747114486E-29, -2.568816543514388222E-44, -4.500000000000000888 ) ) ;
#10814=CARTESIAN_POINT ( 'NONE',  ( -0.8493553515888951910, -0.2812499999999675260, -4.261981763090987307 ) ) ;
#10817=CARTESIAN_POINT ( 'NONE',  ( 0.4121457528842378815, -1.233588562373086672, -4.200139271419963904 ) ) ;
#10830=CARTESIAN_POINT ( 'NONE',  ( -0.3756913567350075311, -4.265625000000119904, -3.800190021185207545 ) ) ;
#10834=CARTESIAN_POINT ( 'NONE',  ( 2.123627735229571822, -1.428750000000023501, 3.175715285003293253 ) ) ;
#10848=TOROIDAL_SURFACE ( 'NONE', #4164, 2.093999815491831562, 0.2500000000000000000 ) ;
#10850=CARTESIAN_POINT ( 'NONE',  ( 3.380062874710183518, -2.647499999999996856, -1.401527478686715344 ) ) ;
#10851=VERTEX_POINT ( 'NONE', #13331 ) ;
#10854=DIRECTION ( 'NONE',  ( -9.422394424380278809E-16, 1.000000000000000000, -0.000000000000000000 ) ) ;
#10861=CARTESIAN_POINT ( 'NONE',  ( -2.598076211353315568, 0.1227504548087345604, 4.500000000000000888 ) ) ;
#10864=CARTESIAN_POINT ( 'NONE',  ( 3.463329978863818770, -3.616249999999970210, -0.6879750677194342856 ) ) ;
#10866=ORIENTED_EDGE ( 'NONE', *, *, #11290, .T. ) ;
#10869=EDGE_CURVE ( 'NONE', #5205, #13967, #4293, .T. ) ;
#10876=CARTESIAN_POINT ( 'NONE',  ( 0.000000000000000000, 0.000000000000000000, 0.000000000000000000 ) ) ;
#10885=CARTESIAN_POINT ( 'NONE',  ( 5.196152422706624918, 2.375000000000013323, -1.265134450516282343E-15 ) ) ;
#10892=FACE_OUTER_BOUND ( 'NONE', #9516, .T. ) ;
#10893=CARTESIAN_POINT ( 'NONE',  ( 1.666359390640659743, -0.1874999999999558131, -4.027044093784315493 ) ) ;
#10894=CARTESIAN_POINT ( 'NONE',  ( 3.296805766952802141, -0.8898385623730955540, 2.707089161679790745 ) ) ;
#10898=DIRECTION ( 'NONE',  ( 1.000000000000000000, 1.067522139062645347E-15, 0.000000000000000000 ) ) ;
#10899=CARTESIAN_POINT ( 'NONE',  ( 4.500000000000000888, 1.148368900306797199E-14, 0.000000000000000000 ) ) ;
#10904=CARTESIAN_POINT ( 'NONE',  ( 0.7448305450414310913, -4.218749999999887201, -3.751694669322447329 ) ) ;
#10915=ORIENTED_EDGE ( 'NONE', *, *, #5650, .F. ) ;
#10920=DIRECTION ( 'NONE',  ( 2.551930889570659960E-15, -1.000000000000000000, -0.000000000000000000 ) ) ;
#10921=CARTESIAN_POINT ( 'NONE',  ( 3.515159614179530490, -2.538124999999942677, 1.067305873498054059 ) ) ;
#10930=CARTESIAN_POINT ( 'NONE',  ( -2.894171431151455032, -0.4995676945082664355, -3.078752850849113099 ) ) ;
#10936=ORIENTED_EDGE ( 'NONE', *, *, #13673, .F. ) ;
#10943=CARTESIAN_POINT ( 'NONE',  ( 0.0009802357451226765411, -1.834999999999918474, -3.766633749593359060 ) ) ;
#10945=CARTESIAN_POINT ( 'NONE',  ( -3.138285373062238648, -4.593749999999839240, 2.098600886432549828 ) ) ;
#10947=DIRECTION ( 'NONE',  ( -9.422394424380278809E-16, 1.000000000000000000, -0.000000000000000000 ) ) ;
#10959=EDGE_CURVE ( 'NONE', #5763, #8567, #5076, .T. ) ;
#10964=DIRECTION ( 'NONE',  ( -1.747085166004344019E-15, 1.000000000000000000, -0.000000000000000000 ) ) ;
#10966=CARTESIAN_POINT ( 'NONE',  ( -0.8236255389490674261, -1.280463562373061359, -4.132840929750037695 ) ) ;
#10972=LINE ( 'NONE', #2907, #11988 ) ;
#10981=SURFACE_SIDE_STYLE ('',( #9955 ) ) ;
#10982=CARTESIAN_POINT ( 'NONE',  ( 0.0009972298945177876170, -4.250000000000088818, -3.820821809411817149 ) ) ;
#10984=CARTESIAN_POINT ( 'NONE',  ( 0.7308567215121246630, -4.780463562373078013, 3.679264497522872102 ) ) ;
#10985=CIRCLE ( 'NONE', #8992, 4.500000000000000888 ) ;
#10986=CARTESIAN_POINT ( 'NONE',  ( 3.783562653031121936, -1.569374999999871845, 0.3712484392075319217 ) ) ;
#10988=AXIS2_PLACEMENT_3D ( 'NONE', #4068, #2588, #10898 ) ;
#10999=CARTESIAN_POINT ( 'NONE',  ( -1.629699455448989389E-14, 8.699999999999999289, 5.655858585055787181E-29 ) ) ;
#11000=CARTESIAN_POINT ( 'NONE',  ( -2.557519727433407386, -2.960000000000007958, -2.558839988362046292 ) ) ;
#11015=VERTEX_POINT ( 'NONE', #10641 ) ;
#11020=CARTESIAN_POINT ( 'NONE',  ( -1.418005212499557466, -2.272500000000021281, 3.426931839692804349 ) ) ;
#11024=CARTESIAN_POINT ( 'NONE',  ( -2.938526230868574896, -4.390625000000237144, -2.412868667173103443 ) ) ;
#11028=CARTESIAN_POINT ( 'NONE',  ( 1.916065064279496746E-15, 7.362499999999997158, 0.000000000000000000 ) ) ;
#11041=CARTESIAN_POINT ( 'NONE',  ( -2.763334307196397166, -5.178749999999838316, 1.847896475581856324 ) ) ;
#11044=CARTESIAN_POINT ( 'NONE',  ( 1.260313249030131866, -5.397499999999716636, 3.044840626206112510 ) ) ;
#11061=AXIS2_PLACEMENT_3D ( 'NONE', #5294, #14660, #7630 ) ;
#11064=CARTESIAN_POINT ( 'NONE',  ( 2.275354997129654055, -2.156249999999973799, -3.407984217092054013 ) ) ;
#11067=CARTESIAN_POINT ( 'NONE',  ( -3.630351441462646545, -3.436713562372988306, -1.502189642148185955 ) ) ;
#11069=EDGE_CURVE ( 'NONE', #11128, #8406, #14682, .T. ) ;
#11074=AXIS2_PLACEMENT_3D ( 'NONE', #11173, #6316, #13288 ) ;
#11080=DIRECTION ( 'NONE',  ( 0.000000000000000000, -0.000000000000000000, -1.000000000000000000 ) ) ;
#11081=CARTESIAN_POINT ( 'NONE',  ( 0.0009802357451110755779, -1.834999999999918474, -3.766633749593359948 ) ) ;
#11086=CARTESIAN_POINT ( 'NONE',  ( -3.461439457045234036, -5.267711698978494894, -0.3686391104329558854 ) ) ;
#11088=CARTESIAN_POINT ( 'NONE',  ( -3.696383486563912246, -0.4995676945082690446, -2.108736548924112331 ) ) ;
#11103=CARTESIAN_POINT ( 'NONE',  ( -1.128754118026385589, -3.703125000000009770, 3.725901868457750954 ) ) ;
#11117=CARTESIAN_POINT ( 'NONE',  ( -3.186695398571379734, -5.131874999999967990, 0.9679749472945999855 ) ) ;
#11120=CARTESIAN_POINT ( 'NONE',  ( -1.792750223658541309, -5.928749999999893383, -2.680858111629535578 ) ) ;
#11128=VERTEX_POINT ( 'NONE', #10807 ) ;
#11133=CARTESIAN_POINT ( 'NONE',  ( -1.508667427112231785, -3.312499999999990674, -3.644952880303303555 ) ) ;
#11146=( LENGTH_UNIT ( ) NAMED_UNIT ( * ) SI_UNIT ( .MILLI., .METRE. ) );
#11148=ORIENTED_EDGE ( 'NONE', *, *, #1091, .F. ) ;
#11149=DIRECTION ( 'NONE',  ( -1.000000000000000000, 0.000000000000000000, 0.000000000000000000 ) ) ;
#11150=CARTESIAN_POINT ( 'NONE',  ( 2.697785604507370927, -1.459999999999946008, 2.699193867783729051 ) ) ;
#11156=DIRECTION ( 'NONE',  ( -1.000000000000000000, -2.459952698498907323E-15, 0.000000000000000000 ) ) ;
#11157=CARTESIAN_POINT ( 'NONE',  ( 1.525801098514460996, -0.4995676945082557219, -3.817740101069251324 ) ) ;
#11169=CARTESIAN_POINT ( 'NONE',  ( 2.949251946438511407, -1.475624999999980647, 2.418581166398158455 ) ) ;
#11171=CARTESIAN_POINT ( 'NONE',  ( -1.460276376564476175, -4.312500000000168754, -3.521769549316223102 ) ) ;
#11173=CARTESIAN_POINT ( 'NONE',  ( -1.006616814747114065E-29, -2.568816543514387226E-44, 0.000000000000000000 ) ) ;
#11175=CARTESIAN_POINT ( 'NONE',  ( 0.8338062855310036658, -0.7812499999999443778, 4.197676506703500010 ) ) ;
#11181=SPHERICAL_SURFACE ( 'NONE', #315, 0.8600000000000014300 ) ;
#11188=CARTESIAN_POINT ( 'NONE',  ( -3.191126515704095556, -6.069374228118336490, -0.3131016245760979699 ) ) ;
#11197=CARTESIAN_POINT ( 'NONE',  ( 2.642398951855386535, -4.475625000000026610, 2.166914421091147069 ) ) ;
#11198=ORIENTED_EDGE ( 'NONE', *, *, #230, .T. ) ;
#11204=CARTESIAN_POINT ( 'NONE',  ( 3.808142666863014281, -3.046875000000033751, -1.156701755244785801 ) ) ;
#11219=DIRECTION ( 'NONE',  ( 1.000000000000000000, 2.459952698498907718E-15, 0.000000000000000000 ) ) ;
#11224=CARTESIAN_POINT ( 'NONE',  ( -3.705025434593251621, -1.038125000000020393, -1.124966067554212801 ) ) ;
#11231=CARTESIAN_POINT ( 'NONE',  ( -2.612410911831650306, -5.223873800609857732, -2.385990627414828147 ) ) ;
#11251=EDGE_CURVE ( 'NONE', #6571, #3303, #9742, .T. ) ;
#11252=CARTESIAN_POINT ( 'NONE',  ( -3.160451915950723389, -4.406249999999939604, -2.110071460981538749 ) ) ;
#11259=CARTESIAN_POINT ( 'NONE',  ( 0.001121683909886545937, -1.249999999999918066, -4.217678074926116238 ) ) ;
#11273=CARTESIAN_POINT ( 'NONE',  ( -3.268702447147800783, -5.116250000000009734, 0.6493246907702930892 ) ) ;
#11275=PLANE ( 'NONE',  #10177 ) ;
#11279=AXIS2_PLACEMENT_3D ( 'NONE', #13898, #9160, #8868 ) ;
#11285=CARTESIAN_POINT ( 'NONE',  ( 4.043635966909349122, -1.968749999999958034, 0.8028061105223156524 ) ) ;
#11290=EDGE_CURVE ( 'NONE', #9311, #953, #2315, .T. ) ;
#11296=AXIS2_PLACEMENT_3D ( 'NONE', #8721, #14538, #13469 ) ;
#11301=CARTESIAN_POINT ( 'NONE',  ( 1.112125432426072313, -1.381875000000161391, 3.661359949638919087 ) ) ;
#11315=CONICAL_SURFACE ( 'NONE', #13790, 4.500000000000000888, 1.396263401595466691 ) ;
#11322=VERTEX_POINT ( 'NONE', #12649 ) ;
#11323=CARTESIAN_POINT ( 'NONE',  ( -0.6922063445227994993, -6.280463562373093112, -3.484636965811530818 ) ) ;
#11324=CARTESIAN_POINT ( 'NONE',  ( 0.001402937982463629916, -1.335000000000034825, 3.832736870811212171 ) ) ;
#11328=CARTESIAN_POINT ( 'NONE',  ( -3.978302601493375334, -2.468750000000105693, -0.7924256976418916354 ) ) ;
#11332=CARTESIAN_POINT ( 'NONE',  ( -2.598076211353319565, 1.678847577293365978, -4.499999999999999112 ) ) ;
#11333=CARTESIAN_POINT ( 'NONE',  ( -1.243836315904764955, -0.7031249999999807931, 4.105705763534058583 ) ) ;
#11347=CARTESIAN_POINT ( 'NONE',  ( 0.3227798623957477964, -5.350624999999817888, 3.285751646651179136 ) ) ;
#11354=CARTESIAN_POINT ( 'NONE',  ( 1.002467944199222138, -0.4995676945082564990, 3.916338062624285410 ) ) ;
#11361=CARTESIAN_POINT ( 'NONE',  ( -4.184567129761759929, -1.500000000000142109, 0.001513272625389735625 ) ) ;
#11364=CARTESIAN_POINT ( 'NONE',  ( -2.167558509990396232, -3.655463562373140185, 3.242140913184852202 ) ) ;
#11375=CARTESIAN_POINT ( 'NONE',  ( 0.7224497989600291437, -2.366250000000003517, 3.625028471221729554 ) ) ;
#11389=CARTESIAN_POINT ( 'NONE',  ( 0.3183433322350087691, -5.819374999999986642, -3.223879781222068086 ) ) ;
#11392=B_SPLINE_CURVE_WITH_KNOTS ( 'NONE', 3,
 ( #15038, #3111, #7848, #6762, #4496, #15186, #12720, #9076, #11482, #9299, #4427, #9147 ),
 .UNSPECIFIED., .F., .F.,
 ( 4, 2, 2, 2, 2, 4 ),
 ( 2.544323688695237330E-07, 0.001342108318545693138, 0.002013035261634103963, 0.002683962204722515222, 0.004025816090899335571, 0.005367669977076155487 ),
 .UNSPECIFIED. ) ;
#11393=ORIENTED_EDGE ( 'NONE', *, *, #7251, .F. ) ;
#11394=CARTESIAN_POINT ( 'NONE',  ( -2.735908675276634838, -6.389838562373163278, -2.243606804512522146 ) ) ;
#11395=CARTESIAN_POINT ( 'NONE',  ( 2.123627735229571822, -1.428750000000023501, 3.175715285003293253 ) ) ;
#11397=CARTESIAN_POINT ( 'NONE',  ( 2.275354997129654055, -2.156249999999973799, -3.407984217092054013 ) ) ;
#11400=CARTESIAN_POINT ( 'NONE',  ( -3.579691249134443698, -0.5937499999999900080, 2.390491442833416080 ) ) ;
#11404=DIRECTION ( 'NONE',  ( 1.000000000000000000, 0.000000000000000000, 0.000000000000000000 ) ) ;
#11411=B_SPLINE_CURVE_WITH_KNOTS ( 'NONE', 3,
 ( #1308, #8299, #6153, #10861 ),
 .UNSPECIFIED., .F., .F.,
 ( 4, 4 ),
 ( 0.01442070979368249156, 0.01702197257837674560 ),
 .UNSPECIFIED. ) ;
#11413=B_SPLINE_CURVE_WITH_KNOTS ( 'NONE', 3,
 ( #7124, #2449, #2085, #6836, #10667, #118, #13247, #10756, #2372, #42, #2605, #7200, #4784, #1447, #6127, #4870, #198, #11558, #922, #11844, #12716, #5017, #6203, #15103 ),
 .UNSPECIFIED., .F., .F.,
 ( 4, 2, 2, 2, 2, 2, 2, 2, 2, 2, 2, 4 ),
 ( 0.000000000000000000, 0.0008863986295625844031, 0.001329597944343876821, 0.001772797259125169240, 0.002659195888687754077, 0.003102395203469047145, 0.003545594518250340214, 0.004431993147812924617, 0.005318391777375509888, 0.005761591092156802089, 0.006204790406938094291, 0.007091189036500678694 ),
 .UNSPECIFIED. ) ;
#11414=CARTESIAN_POINT ( 'NONE',  ( 0.9968050443165101804, -4.381875000000003517, 3.281628308787421400 ) ) ;
#11418=PLANE ( 'NONE',  #7249 ) ;
#11426=CARTESIAN_POINT ( 'NONE',  ( 3.136514378097080780, -4.647499999999995524, -1.298252083346796759 ) ) ;
#11435=CARTESIAN_POINT ( 'NONE',  ( 0.8105829119240891556, -1.781250000000002887, 4.067378511145360420 ) ) ;
#11437=CARTESIAN_POINT ( 'NONE',  ( 3.809485474318313081, -3.046088562373004738, -1.154500326837077484 ) ) ;
#11439=CARTESIAN_POINT ( 'NONE',  ( -1.096602777094355814E-14, 4.297149196226271783, 0.000000000000000000 ) ) ;
#11445=CARTESIAN_POINT ( 'NONE',  ( -1.705466066262326307E-14, 9.560000000000000497, 5.619086434621074034E-29 ) ) ;
#11449=CIRCLE ( 'NONE', #12953, 2.431404194366992400 ) ;
#11453=CARTESIAN_POINT ( 'NONE',  ( 3.768993168962233575, -0.5381249999999744293, 1.141810966380977455 ) ) ;
#11456=CARTESIAN_POINT ( 'NONE',  ( 0.0009802357451226765411, -1.834999999999918474, -3.766633749593359060 ) ) ;
#11475=CARTESIAN_POINT ( 'NONE',  ( -1.031947532464913664, -6.296088562372862185, -3.397346913929182755 ) ) ;
#11476=CARTESIAN_POINT ( 'NONE',  ( -3.795858268372354516, -1.053749999999936460, -0.7536008350790791566 ) ) ;
#11478=CARTESIAN_POINT ( 'NONE',  ( -1.920019182618211584, -2.328124999999937383, -3.594387849940205104 ) ) ;
#11482=CARTESIAN_POINT ( 'NONE',  ( 4.342069816296828755, 2.307268873417431809, 1.479314468162619578 ) ) ;
#11483=CARTESIAN_POINT ( 'NONE',  ( 3.757405615841324042, -0.9218749999999823475, 2.009662442622283773 ) ) ;
#11485=CIRCLE ( 'NONE', #3567, 4.401041666666736241 ) ;
#11497=CARTESIAN_POINT ( 'NONE',  ( 1.879752899984456160, -4.741249999999911147, -2.811701655874830230 ) ) ;
#11502=CARTESIAN_POINT ( 'NONE',  ( -0.7619189956411019926, -0.4995676945082610509, 4.033706137351277476 ) ) ;
#11514=CARTESIAN_POINT ( 'NONE',  ( -3.245221319803801130, -1.390624999999827915, -2.664727821046819489 ) ) ;
#11517=CARTESIAN_POINT ( 'NONE',  ( 1.534191850248811884, -2.811713562373064690, 3.706628987441562995 ) ) ;
#11531=CARTESIAN_POINT ( 'NONE',  ( 3.280408283555247717, -0.4912499999999521139, 2.190169342145847242 ) ) ;
#11533=AXIS2_PLACEMENT_3D ( 'NONE', #8445, #4024, #8752 ) ;
#11535=CARTESIAN_POINT ( 'NONE',  ( 3.722330097189530562, -1.616249999999942899, -0.7418360188101028596 ) ) ;
#11549=CARTESIAN_POINT ( 'NONE',  ( 1.903042727507281651, -4.428749999999965326, 2.845810502761935812 ) ) ;
#11557=CARTESIAN_POINT ( 'NONE',  ( -3.686556889460864461, -0.1475000000000124822, 1.525885089196999056 ) ) ;
#11558=CARTESIAN_POINT ( 'NONE',  ( -3.050151834521379168, -5.307756522154472023, 1.562533256231358747 ) ) ;
#11559=CARTESIAN_POINT ( 'NONE',  ( 2.623679764461153141, -1.859375000000051070, 3.198691315062023310 ) ) ;
#11584=DIRECTION ( 'NONE',  ( -0.4226182617406989417, -0.9063077870366502697, 5.175581015019663092E-17 ) ) ;
#11592=CARTESIAN_POINT ( 'NONE',  ( -2.667636957649788698, -1.359375000000169198, -3.248130456407447575 ) ) ;
#11594=CARTESIAN_POINT ( 'NONE',  ( 1.929669553967771956, -2.171088562373077124, -3.613309278117248002 ) ) ;
#11608=CARTESIAN_POINT ( 'NONE',  ( -1.153796164589674156, -0.2881249999999724309, 3.799958344797443210 ) ) ;
#11610=CARTESIAN_POINT ( 'NONE',  ( -0.3615547238505233407, -2.319374999999934239, 3.684823279838126187 ) ) ;
#11617=CARTESIAN_POINT ( 'NONE',  ( 0.000000000000000000, 0.000000000000000000, 0.000000000000000000 ) ) ;
#11626=ORIENTED_EDGE ( 'NONE', *, *, #10743, .F. ) ;
#11631=CARTESIAN_POINT ( 'NONE',  ( -3.630878219354529257, -4.452338562373184594, -1.102448361598825644 ) ) ;
#11632=CARTESIAN_POINT ( 'NONE',  ( -3.563362751979704868, -1.147500000000009734, 1.477520127916053472 ) ) ;
#11633=CARTESIAN_POINT ( 'NONE',  ( 3.091873775341146491, -2.890625000000027534, 2.538798244104332191 ) ) ;
#11635=DIRECTION ( 'NONE',  ( -1.000000000000000000, -2.551930889570659960E-15, 0.000000000000000000 ) ) ;
#11637=CARTESIAN_POINT ( 'NONE',  ( -2.598076211353320453, 2.374999999999993339, 4.500000000000000888 ) ) ;
#11643=VERTEX_POINT ( 'NONE', #13274 ) ;
#11646=DIRECTION ( 'NONE',  ( 1.000000000000000000, 0.000000000000000000, -0.000000000000000000 ) ) ;
#11647=CARTESIAN_POINT ( 'NONE',  ( -0.2250800285832887659, 2.375126720995723417, -4.499999999999999112 ) ) ;
#11649=B_SPLINE_CURVE_WITH_KNOTS ( 'NONE', 3,
 ( #8829, #7680, #597, #5350 ),
 .UNSPECIFIED., .F., .F.,
 ( 4, 4 ),
 ( 2.309401076754191683E-07, 0.002598307151460989371 ),
 .UNSPECIFIED. ) ;
#11651=CARTESIAN_POINT ( 'NONE',  ( 3.897114317029974018, 9.945166405816858860E-15, -2.250000000000001332 ) ) ;
#11657=ORIENTED_EDGE ( 'NONE', *, *, #10413, .T. ) ;
#11660=CARTESIAN_POINT ( 'NONE',  ( -4.010754789764311212, -1.453125000000109912, -1.215065766439024975 ) ) ;
#11662=CARTESIAN_POINT ( 'NONE',  ( -1.540128476469153185, -2.686713562373115760, 3.722025193358375894 ) ) ;
#11672=CARTESIAN_POINT ( 'NONE',  ( 3.315864351079437888, -5.143616724908924631, -1.547231645668555533 ) ) ;
#11677=CARTESIAN_POINT ( 'NONE',  ( -2.837724166816209426, -5.390625000000070166, -2.327111198264740999 ) ) ;
#11680=CARTESIAN_POINT ( 'NONE',  ( -3.733522804429754149, -2.085000000000140741, 0.001371824453762974898 ) ) ;
#11695=AXIS2_PLACEMENT_3D ( 'NONE', #13608, #7714, #12439 ) ;
#11698=CARTESIAN_POINT ( 'NONE',  ( -0.9755776780686776783, -4.881874999999863185, -3.218989981404325462 ) ) ;
#11702=CARTESIAN_POINT ( 'NONE',  ( 2.889335172541571684, -4.889838562373118869, 2.369440177208199660 ) ) ;
#11713=B_SPLINE_CURVE_WITH_KNOTS ( 'NONE', 3,
 ( #5584, #10288, #1523, #47, #13171, #13251, #9739, #3931, #7282, #9821, #4791, #2530, #6278, #12006 ),
 .UNSPECIFIED., .F., .F.,
 ( 4, 2, 2, 2, 2, 2, 4 ),
 ( 0.002345953150261289536, 0.002784084228693953569, 0.003222215307126618036, 0.004098477463991946970, 0.004536608542424611437, 0.004974739620857275037, 0.005851001777722601369 ),
 .UNSPECIFIED. ) ;
#11716=CARTESIAN_POINT ( 'NONE',  ( 3.009749400183384882, -4.506874999999939568, 1.609730366092098075 ) ) ;
#11727=CARTESIAN_POINT ( 'NONE',  ( -0.9979582191391829227, -4.288125000000008846, 3.294238300096191452 ) ) ;
#11730=CARTESIAN_POINT ( 'NONE',  ( 3.721607743032638638, -5.000000000000047073, 0.0009661164014421728431 ) ) ;
#11748=CARTESIAN_POINT ( 'NONE',  ( 3.069693586880715142, -3.108588562373168163, -2.521103932842495343 ) ) ;
#11751=CARTESIAN_POINT ( 'NONE',  ( 5.196152422706626695, 1.678847577293385296, -1.115338501812287204E-15 ) ) ;
#11760=CARTESIAN_POINT ( 'NONE',  ( 3.915012698312750228, -0.5693749999999865308, 0.3866328316385075348 ) ) ;
#11764=CARTESIAN_POINT ( 'NONE',  ( -2.084927739720960016, -1.928749999999817888, -3.122072247380865306 ) ) ;
#11771=CIRCLE ( 'NONE', #9536, 0.8000000000000113687 ) ;
#11772=EDGE_LOOP ( 'NONE', ( #7304, #8680, #13336 ) ) ;
#11777=CARTESIAN_POINT ( 'NONE',  ( -2.211816241884709822, -3.944375000000018172, -2.696513105594181336 ) ) ;
#11778=ORIENTED_EDGE ( 'NONE', *, *, #13630, .F. ) ;
#11782=CARTESIAN_POINT ( 'NONE',  ( 3.702328265034185772, -5.014838562373222786, -0.3636771760147958776 ) ) ;
#11794=CARTESIAN_POINT ( 'NONE',  ( -2.189584623831577037, -4.225624999999936016, 2.666627758504775958 ) ) ;
#11806=CARTESIAN_POINT ( 'NONE',  ( -2.773226354234704427, -3.194375000000006182, 2.274732928208734961 ) ) ;
#11808=AXIS2_PLACEMENT_3D ( 'NONE', #9180, #8029, #15149 ) ;
#11814=CARTESIAN_POINT ( 'NONE',  ( -4.296774773080532128, -0.4990699899015805241, -0.003879984233104640575 ) ) ;
#11825=CARTESIAN_POINT ( 'NONE',  ( -3.065271248674581006, -0.3749999999999933942, -3.063065156281021384 ) ) ;
#11828=CARTESIAN_POINT ( 'NONE',  ( -3.040116134197859754, -0.6242135623732079086, 3.042307828174728446 ) ) ;
#11834=EDGE_LOOP ( 'NONE', ( #4953, #11876, #13128 ) ) ;
#11840=CARTESIAN_POINT ( 'NONE',  ( -3.920035875790600421, -3.499999999999977796, -0.001028343392498549860 ) ) ;
#11844=CARTESIAN_POINT ( 'NONE',  ( -3.238071519113512320, -5.298747598780473744, 1.157691333774819364 ) ) ;
#11857=CARTESIAN_POINT ( 'NONE',  ( 2.315514200798128197, -2.725624999999891607, -2.819975302942780981 ) ) ;
#11861=CARTESIAN_POINT ( 'NONE',  ( -1.458314181602024417, -4.311713562372998965, -3.523281483662707547 ) ) ;
#11872=CARTESIAN_POINT ( 'NONE',  ( -3.319861881881159160, -3.147500000000079456, 1.374129751973758307 ) ) ;
#11876=ORIENTED_EDGE ( 'NONE', *, *, #8487, .T. ) ;
#11880=CARTESIAN_POINT ( 'NONE',  ( 0.3668491701747067513, -4.765624999999817923, 3.734637934618871391 ) ) ;
#11881=CARTESIAN_POINT ( 'NONE',  ( -0.9013897962190543511, 2.290928418201631622, -4.499999999999999112 ) ) ;
#11897=EDGE_CURVE ( 'NONE', #8008, #11322, #9445, .T. ) ;
#11901=CARTESIAN_POINT ( 'NONE',  ( -0.4121457528836308115, -1.264838562373080677, -4.196025130973226602 ) ) ;
#11912=DIRECTION ( 'NONE',  ( -1.000000000000000000, -1.783664229908549233E-15, 0.000000000000000000 ) ) ;
#11916=CARTESIAN_POINT ( 'NONE',  ( 1.127871658241229147, -3.796875000000003553, 3.713209756639876069 ) ) ;
#11919=CARTESIAN_POINT ( 'NONE',  ( 2.769370807496521980, -0.7100000000000333822, -2.767918543042355850 ) ) ;
#11932=CARTESIAN_POINT ( 'NONE',  ( 3.109021928378527644, -3.663124999999927578, -1.660781358203028413 ) ) ;
#11935=VERTEX_POINT ( 'NONE', #3313 ) ;
#11940=B_SPLINE_CURVE_WITH_KNOTS ( 'NONE', 3,
 ( #7679, #3790, #11086, #14402, #12165, #13265, #14567, #2775, #458, #8603, #11231, #12403, #6220, #7528, #1765, #9981, #2632, #286, #1616, #12100, #14486, #5196, #13347, #4100, #9907, #14633, #2705, #7449, #373, #8747 ),
 .UNSPECIFIED., .F., .F.,
 ( 4, 2, 2, 2, 2, 2, 2, 2, 2, 2, 2, 2, 2, 2, 4 ),
 ( 0.007091189036500678694, 0.007645091323452510995, 0.008198993610404343296, 0.008752895897356175597, 0.009306798184308006164, 0.009860700471259838465, 0.01041460275821166903, 0.01096850504516350133, 0.01152240733211533363, 0.01207630961906716247, 0.01263021190601899477, 0.01373801647992265763, 0.01484582105382632224, 0.01539972334077815454, 0.01595362562772998510 ),
 .UNSPECIFIED. ) ;
#11944=CARTESIAN_POINT ( 'NONE',  ( 1.033118776976089670, -3.381875000000070131, 3.408891928937246796 ) ) ;
#11954=CARTESIAN_POINT ( 'NONE',  ( 3.535094671665813593, -3.584999999999991083, -0.001309597400350119394 ) ) ;
#11965=DIRECTION ( 'NONE',  ( 2.551930889570659960E-15, -1.000000000000000000, -0.000000000000000000 ) ) ;
#11973=B_SPLINE_CURVE_WITH_KNOTS ( 'NONE', 3,
 ( #8542, #4044, #14585, #3893 ),
 .UNSPECIFIED., .F., .F.,
 ( 4, 4 ),
 ( 0.01181595095932581191, 0.01442070979368249156 ),
 .UNSPECIFIED. ) ;
#11975=CARTESIAN_POINT ( 'NONE',  ( 3.088407327495258148, -0.1250000000000329736, -3.086755025163618882 ) ) ;
#11978=CARTESIAN_POINT ( 'NONE',  ( 1.637824775874881178, -0.8117135623732008032, 3.950029390179780719 ) ) ;
#11986=ORIENTED_EDGE ( 'NONE', *, *, #10187, .F. ) ;
#11988=VECTOR ( 'NONE', #8564, 1000.000000000000000 ) ;
#11994=CARTESIAN_POINT ( 'NONE',  ( -2.415777803760090325, -4.359374999999756639, -2.941435367455751848 ) ) ;
#11999=CARTESIAN_POINT ( 'NONE',  ( 3.768993168962329054, -0.5381249999999744293, 1.141810966380977455 ) ) ;
#12001=AXIS2_PLACEMENT_3D ( 'NONE', #1219, #9587, #10677 ) ;
#12005=DIRECTION ( 'NONE',  ( -2.551930889570660354E-15, 1.000000000000000000, 0.000000000000000000 ) ) ;
#12006=CARTESIAN_POINT ( 'NONE',  ( 1.682902201845278611, -5.420849775684215999, 2.811263474311217259 ) ) ;
#12016=CARTESIAN_POINT ( 'NONE',  ( -3.535952561574606801, -3.053750000000104770, -0.7042925846621640451 ) ) ;
#12030=CARTESIAN_POINT ( 'NONE',  ( 1.342127543875233808, -3.772500000000060805, -3.243584335895732362 ) ) ;
#12038=CONICAL_SURFACE ( 'NONE', #5098, 4.500000000000000888, 1.396263401595466691 ) ;
#12040=CARTESIAN_POINT ( 'NONE',  ( -3.527726845254099075, -3.116249999999919140, 0.7030635791094290710 ) ) ;
#12041=DIRECTION ( 'NONE',  ( 1.000000000000000000, 9.422394424380278809E-16, 0.000000000000000000 ) ) ;
#12053=AXIS2_PLACEMENT_3D ( 'NONE', #14372, #1430, #13537 ) ;
#12060=CARTESIAN_POINT ( 'NONE',  ( -4.230142555718267694, -0.5304635623730820093, 0.8430117587971442950 ) ) ;
#12064=CIRCLE ( 'NONE', #11279, 4.500000000000000888 ) ;
#12077=CARTESIAN_POINT ( 'NONE',  ( -1.128754118026385589, -3.703125000000009770, 3.725901868457750954 ) ) ;
#12079=CIRCLE ( 'NONE', #14299, 4.500000000000000888 ) ;
#12080=CARTESIAN_POINT ( 'NONE',  ( 3.372444421885775423, -0.4995676945082423992, 2.006840812041871924 ) ) ;
#12094=CARTESIAN_POINT ( 'NONE',  ( 2.229831107420913838, -3.725624999999957776, -2.719112200499365528 ) ) ;
#12100=CARTESIAN_POINT ( 'NONE',  ( -0.3745637740607890565, -5.173691999402833197, -3.583788933605721816 ) ) ;
#12108=EDGE_CURVE ( 'NONE', #9101, #4411, #3261, .T. ) ;
#12113=ORIENTED_EDGE ( 'NONE', *, *, #5274, .F. ) ;
#12115=CIRCLE ( 'NONE', #472, 0.5000000000000000000 ) ;
#12117=CARTESIAN_POINT ( 'NONE',  ( -2.896649075160178111, -1.975624999999826548, -2.378478989283399514 ) ) ;
#12118=CARTESIAN_POINT ( 'NONE',  ( -3.466918327573330849, -3.421874999999993339, -1.851480974780293387 ) ) ;
#12127=AXIS2_PLACEMENT_3D ( 'NONE', #8811, #1450, #6204 ) ;
#12132=CARTESIAN_POINT ( 'NONE',  ( 3.270563417710623089, -5.585000000000047038, 0.0008246681304770143647 ) ) ;
#12134=CARTESIAN_POINT ( 'NONE',  ( -1.593139518311427194, -1.686713562373179487, 3.843294861269374252 ) ) ;
#12144=CARTESIAN_POINT ( 'NONE',  ( 3.568675334318531345, -3.937499999999699796, 1.476665218992084139 ) ) ;
#12146=CARTESIAN_POINT ( 'NONE',  ( -3.350768293094503303, -4.421088562373000741, -1.789444311552624400 ) ) ;
#12147=CARTESIAN_POINT ( 'NONE',  ( -3.204583014436136690, -1.178749999999988640, 2.140022251743640691 ) ) ;
#12150=LINE ( 'NONE', #14695, #9970 ) ;
#12158=CARTESIAN_POINT ( 'NONE',  ( -3.527726845254099519, -3.116249999999919140, 0.7030635791094292930 ) ) ;
#12165=CARTESIAN_POINT ( 'NONE',  ( -3.372107705793691235, -5.256639709918796477, -0.9200269475832475452 ) ) ;
#12168=CARTESIAN_POINT ( 'NONE',  ( -1.006616814747114065E-29, -2.568816543514387226E-44, 0.000000000000000000 ) ) ;
#12182=CARTESIAN_POINT ( 'NONE',  ( 3.515159614179530045, -2.538124999999942677, 1.067305873498098912 ) ) ;
#12186=CARTESIAN_POINT ( 'NONE',  ( -3.018109139697564114, -3.609375000000057732, 2.478742592228960095 ) ) ;
#12187=DIRECTION ( 'NONE',  ( 0.1305261922200519342, 0.9914448613738104932, 1.598484835071818104E-17 ) ) ;
#12190=CARTESIAN_POINT ( 'NONE',  ( -4.781720599710164166, 2.058119353682382524, -0.7178169737032800146 ) ) ;
#12200=EDGE_LOOP ( 'NONE', ( #5593, #14256, #6787, #5135 ) ) ;
#12205=CARTESIAN_POINT ( 'NONE',  ( 2.894038744318264023, -5.506874999999972431, 1.545501402921600764 ) ) ;
#12216=CIRCLE ( 'NONE', #312, 0.8000000000000113687 ) ;
#12220=CARTESIAN_POINT ( 'NONE',  ( 1.567576417386008947, -2.187499999999996447, -3.781634774997608250 ) ) ;
#12241=CARTESIAN_POINT ( 'NONE',  ( -0.3615547238505232852, -2.319374999999934239, 3.684823279838035592 ) ) ;
#12251=AXIS2_PLACEMENT_3D ( 'NONE', #9828, #6441, #8663 ) ;
#12252=CIRCLE ( 'NONE', #10753, 3.250000000000016431 ) ;
#12253=ADVANCED_FACE ( 'NONE', ( #8185 ), #4464, .F. ) ;
#12263=VERTEX_POINT ( 'NONE', #13925 ) ;
#12265=CARTESIAN_POINT ( 'NONE',  ( 3.359686712365983929, -1.506874999999983755, 1.796916873358819222 ) ) ;
#12266=VECTOR ( 'NONE', #4984, 1000.000000000000000 ) ;
#12267=CARTESIAN_POINT ( 'NONE',  ( 3.407468303614469285, -3.921874999999769074, 1.822475935421856708 ) ) ;
#12269=DIRECTION ( 'NONE',  ( 1.000000000000000000, 0.000000000000000000, -6.982962677686266711E-15 ) ) ;
#12286=CARTESIAN_POINT ( 'NONE',  ( -0.6461339251375918247, -5.303750000000252207, 3.244047683681893890 ) ) ;
#12287=CARTESIAN_POINT ( 'NONE',  ( 2.729225460314726348, -5.491250000000120757, 1.824606648063345826 ) ) ;
#12299=ORIENTED_EDGE ( 'NONE', *, *, #3081, .T. ) ;
#12304=ORIENTED_EDGE ( 'NONE', *, *, #2953, .T. ) ;
#12307=CARTESIAN_POINT ( 'NONE',  ( -0.3862366009529625832, -3.265625000000082601, -3.932116680993492874 ) ) ;
#12310=CARTESIAN_POINT ( 'NONE',  ( -0.7578321119627449143, -3.717963562373217012, 3.817165255294980408 ) ) ;
#12311=CARTESIAN_POINT ( 'NONE',  ( -1.151041666666718033, 7.362499999999999822, -1.409619492768633328E-16 ) ) ;
#12325=CARTESIAN_POINT ( 'NONE',  ( -3.284049251726959717, -2.163124999999908482, 1.754264853118110645 ) ) ;
#12327=AXIS2_PLACEMENT_3D ( 'NONE', #13908, #12827, #10333 ) ;
#12331=CARTESIAN_POINT ( 'NONE',  ( 0.6247369625527983139, -0.4995676945082569986, -4.086673213606401234 ) ) ;
#12342=ORIENTED_EDGE ( 'NONE', *, *, #6637, .T. ) ;
#12345=CARTESIAN_POINT ( 'NONE',  ( 2.100337907687909400, -1.741249999999995968, -3.141606438102765075 ) ) ;
#12348=CARTESIAN_POINT ( 'NONE',  ( 3.837491448225466062, -3.984374999999830802, 0.3765428855677108166 ) ) ;
#12353=DIRECTION ( 'NONE',  ( 9.422394424380278809E-16, -1.000000000000000000, 0.000000000000000000 ) ) ;
#12359=CARTESIAN_POINT ( 'NONE',  ( -2.093999815491831562, 9.249999999999998224, 2.564410171457219719E-16 ) ) ;
#12364=CARTESIAN_POINT ( 'NONE',  ( -3.146746057716334199, -6.053749999999687326, -0.6267477053013468247 ) ) ;
#12366=ADVANCED_FACE ( 'NONE', ( #10270 ), #3039, .F. ) ;
#12368=CARTESIAN_POINT ( 'NONE',  ( 0.3183433322350289751, -5.819374999999986642, -3.223879781222067642 ) ) ;
#12375=CARTESIAN_POINT ( 'NONE',  ( -2.589953986283601850, -4.975625000000236220, -2.126619835350766152 ) ) ;
#12382=CARTESIAN_POINT ( 'NONE',  ( 0.7730394778201963302, -3.218749999999914735, -3.881000975522858720 ) ) ;
#12383=EDGE_LOOP ( 'NONE', ( #633, #5363, #9310 ) ) ;
#12386=EDGE_CURVE ( 'NONE', #5514, #13967, #11449, .T. ) ;
#12399=CARTESIAN_POINT ( 'NONE',  ( -3.579091221414612445, -2.038125000000108322, -1.084269867492464678 ) ) ;
#12403=CARTESIAN_POINT ( 'NONE',  ( -2.355616408154719732, -5.216657250684392011, -2.652406391797293761 ) ) ;
#12417=CARTESIAN_POINT ( 'NONE',  ( 1.740706783794652379, -2.413124999999917808, 3.253752085064650412 ) ) ;
#12419=CARTESIAN_POINT ( 'NONE',  ( -3.711107677420292905, -4.531250000000010658, 0.7371803430742600582 ) ) ;
#12422=DIRECTION ( 'NONE',  ( 2.551930889570659960E-15, -1.000000000000000000, -0.000000000000000000 ) ) ;
#12423=CARTESIAN_POINT ( 'NONE',  ( 2.013502677559834808, -0.8281249999998109290, 3.769415173278118480 ) ) ;
#12428=DIRECTION ( 'NONE',  ( 1.000000000000000000, 0.000000000000000000, -1.224646799147352468E-16 ) ) ;
#12436=CARTESIAN_POINT ( 'NONE',  ( -3.146746057716333755, -6.053749999999687326, -0.6267477053013468247 ) ) ;
#12439=DIRECTION ( 'NONE',  ( -1.000000000000000000, -1.747085166004344019E-15, 0.000000000000000000 ) ) ;
#12444=CARTESIAN_POINT ( 'NONE',  ( -2.933994605034232706, -5.163125000000027498, 1.567297863280144865 ) ) ;
#12447=EDGE_CURVE ( 'NONE', #14595, #502, #2661, .T. ) ;
#12448=AXIS2_PLACEMENT_3D ( 'NONE', #767, #4497, #15109 ) ;
#12453=CARTESIAN_POINT ( 'NONE',  ( 3.641945650916532884, -1.921875000000019540, 1.944964469737308299 ) ) ;
#12456=CARTESIAN_POINT ( 'NONE',  ( -3.447875558419448705, -3.577338562373083342, 1.844546225587363031 ) ) ;
#12460=CARTESIAN_POINT ( 'NONE',  ( 2.598076211353314235, 0.1227504548087474667, -4.499999999999999112 ) ) ;
#12462=CARTESIAN_POINT ( 'NONE',  ( 0.9018160986460356243, 2.304554878308276766, 4.500000000000000000 ) ) ;
#12473=CARTESIAN_POINT ( 'NONE',  ( -2.463482987169076210, -0.9443750000000532552, -3.003366100166338093 ) ) ;
#12482=DIRECTION ( 'NONE',  ( 1.000000000000000000, 2.551930889570660354E-15, 0.000000000000000000 ) ) ;
#12496=ORIENTED_EDGE ( 'NONE', *, *, #5174, .T. ) ;
#12498=CARTESIAN_POINT ( 'NONE',  ( -3.508963762376760442, -6.483587779271561935, -0.3443070125793121217 ) ) ;
#12499=CARTESIAN_POINT ( 'NONE',  ( -0.7729260235471533402, -0.3037499999998679590, 3.893172034236888290 ) ) ;
#12502=CARTESIAN_POINT ( 'NONE',  ( 3.641945650916532884, -1.921875000000019540, 1.944964469737308299 ) ) ;
#12507=CARTESIAN_POINT ( 'NONE',  ( -3.663887442738355205, 2.356280171323974937, -2.653960795963570707 ) ) ;
#12508=CARTESIAN_POINT ( 'NONE',  ( 0.8221312990109845842, -1.218750000000059952, -4.140949732771461278 ) ) ;
#12513=CARTESIAN_POINT ( 'NONE',  ( -4.763139720814411504, 0.04639863247562013571, 0.7499999999999986677 ) ) ;
#12519=CARTESIAN_POINT ( 'NONE',  ( 2.516189350642509037, -5.694375000000295728, -2.066564183454873138 ) ) ;
#12524=CARTESIAN_POINT ( 'NONE',  ( -1.623800369386649400, -0.4995676945082628828, 3.803957840413579206 ) ) ;
#12526=CARTESIAN_POINT ( 'NONE',  ( 1.879752899984456160, -4.741249999999911147, -2.811701655874830230 ) ) ;
#12532=CARTESIAN_POINT ( 'NONE',  ( 3.968938162104017842, -2.984375000000153211, 0.3919611025626033030 ) ) ;
#12534=CARTESIAN_POINT ( 'NONE',  ( 2.152085272744272526, -3.842963562373026942, 3.222648864007900293 ) ) ;
#12538=ADVANCED_FACE ( 'NONE', ( #3427 ), #9715, .T. ) ;
#12544=CARTESIAN_POINT ( 'NONE',  ( -3.464101615137753942, -9.164895919936631821E-15, 2.999999999999998668 ) ) ;
#12547=CARTESIAN_POINT ( 'NONE',  ( 1.403561989263863629E-14, -5.500000000000003553, 0.000000000000000000 ) ) ;
#12552=CARTESIAN_POINT ( 'NONE',  ( 3.722330097189531006, -1.616249999999942899, -0.7418360188101490449 ) ) ;
#12570=EDGE_LOOP ( 'NONE', ( #8387, #2462, #11657, #9157 ) ) ;
#12574=CARTESIAN_POINT ( 'NONE',  ( 1.033028120569788211, -6.202338562373084230, -3.409978924178418858 ) ) ;
#12575=CARTESIAN_POINT ( 'NONE',  ( -3.705025434593251177, -1.038125000000020393, -1.124966067554165727 ) ) ;
#12578=CARTESIAN_POINT ( 'NONE',  ( 1.536269025742735383, -2.812500000000037303, 3.705069426614713723 ) ) ;
#12585=CARTESIAN_POINT ( 'NONE',  ( 3.803621785104590794E-17, 9.355654565435173708, 0.000000000000000000 ) ) ;
#12587=CARTESIAN_POINT ( 'NONE',  ( -9.797174393178998714E-17, 9.500000000000000000, 0.000000000000000000 ) ) ;
#12589=CARTESIAN_POINT ( 'NONE',  ( -3.897114317029974462, -9.945166405816860437E-15, 2.249999999999999112 ) ) ;
#12602=CARTESIAN_POINT ( 'NONE',  ( 0.0008557816480155369665, -4.835000000000089670, -3.369777484087370212 ) ) ;
#12608=CARTESIAN_POINT ( 'NONE',  ( 0.8221312990109845842, -1.218750000000059952, -4.140949732771461278 ) ) ;
#12610=CARTESIAN_POINT ( 'NONE',  ( -1.561832126663101450, -2.311713562373265862, -3.766729512901092480 ) ) ;
#12621=CARTESIAN_POINT ( 'NONE',  ( -3.978984329191358693, -0.08500000000000000611, -3.334211887901014441E-13 ) ) ;
#12623=ADVANCED_FACE ( 'NONE', ( #7234 ), #6089, .F. ) ;
#12634=CARTESIAN_POINT ( 'NONE',  ( 2.516189350642509481, -5.694375000000295728, -2.066564183454791870 ) ) ;
#12638=CARTESIAN_POINT ( 'NONE',  ( 3.429681579265138947, -6.046088562373067354, -1.039418128961893117 ) ) ;
#12639=CARTESIAN_POINT ( 'NONE',  ( -0.7612222386588485268, -0.8662499999999671019, -3.819631723157196568 ) ) ;
#12641=CARTESIAN_POINT ( 'NONE',  ( -4.030856054181176873, -2.515624999999848121, 0.3959303163381804880 ) ) ;
#12646=CARTESIAN_POINT ( 'NONE',  ( 1.991706217211437036, -1.171874999999983347, -3.729459312589495923 ) ) ;
#12648=PLANE ( 'NONE',  #13050 ) ;
#12649=CARTESIAN_POINT ( 'NONE',  ( 4.362044368365340929, 1.127570259384924611E-14, 5.341963673457352387E-16 ) ) ;
#12659=EDGE_CURVE ( 'NONE', #10438, #11322, #6239, .T. ) ;
#12671=ORIENTED_EDGE ( 'NONE', *, *, #7893, .F. ) ;
#12675=CARTESIAN_POINT ( 'NONE',  ( 4.172905853428635403, -0.9687499999999248379, 0.8311981373062848899 ) ) ;
#12677=CARTESIAN_POINT ( 'NONE',  ( 3.525795616442236824, -2.921088562373113540, 1.882927806498691403 ) ) ;
#12686=CARTESIAN_POINT ( 'NONE',  ( 2.598076211353309350, 2.375000000000006661, 4.500000000000000000 ) ) ;
#12691=CARTESIAN_POINT ( 'NONE',  ( 3.567009421182318896, -4.953124999999990230, 1.083052099369142818 ) ) ;
#12694=CARTESIAN_POINT ( 'NONE',  ( -3.115386749435359093, -1.991250000000079678, -2.079980318098562098 ) ) ;
#12698=CARTESIAN_POINT ( 'NONE',  ( 3.884135718427222717, -0.4995676945082492271, -1.024675529164014609 ) ) ;
#12707=CARTESIAN_POINT ( 'NONE',  ( -3.313940955170608493, -4.131874999999921805, 1.004348227522814829 ) ) ;
#12712=ORIENTED_EDGE ( 'NONE', *, *, #8062, .T. ) ;
#12714=CARTESIAN_POINT ( 'NONE',  ( 1.148200974759891579, -0.3818749999999526135, 3.788695824010786861 ) ) ;
#12716=CARTESIAN_POINT ( 'NONE',  ( -3.288344415138346744, -5.295814349376151142, 1.018963235593165262 ) ) ;
#12720=CARTESIAN_POINT ( 'NONE',  ( 3.778928804394611873, 2.374507716408110092, 2.454703312603006005 ) ) ;
#12736=CARTESIAN_POINT ( 'NONE',  ( -2.189584623831577037, -4.225624999999936016, 2.666627758504775958 ) ) ;
#12755=CARTESIAN_POINT ( 'NONE',  ( 2.374332146000840194, -0.8437500000000230926, 3.550666350934340354 ) ) ;
#12756=VERTEX_POINT ( 'NONE', #14877 ) ;
#12757=ADVANCED_FACE ( 'NONE', ( #7697 ), #7845, .F. ) ;
#12758=CARTESIAN_POINT ( 'NONE',  ( -2.262274296814194230, -2.342963562372911923, -3.387670398104518199 ) ) ;
#12769=ORIENTED_EDGE ( 'NONE', *, *, #10364, .F. ) ;
#12772=CARTESIAN_POINT ( 'NONE',  ( 1.515516452534993119, -0.3975000000001072675, 3.655012690611889159 ) ) ;
#12775=CARTESIAN_POINT ( 'NONE',  ( -3.586083906644841779, -3.069375000000151399, -0.3518610084925551384 ) ) ;
#12786=CARTESIAN_POINT ( 'NONE',  ( 4.500000000000000888, 1.148368900306797357E-14, 0.000000000000000000 ) ) ;
#12789=ORIENTED_EDGE ( 'NONE', *, *, #9724, .F. ) ;
#12794=CARTESIAN_POINT ( 'NONE',  ( -2.502742494678076746, -6.374213562373193476, -2.504028389392794374 ) ) ;
#12796=CARTESIAN_POINT ( 'NONE',  ( 3.915012698312653860, -0.5693749999999865308, 0.3866328316385073127 ) ) ;
#12797=CARTESIAN_POINT ( 'NONE',  ( -0.4056240317154969355, -1.734374999999933831, 4.133709567805635920 ) ) ;
#12799=CARTESIAN_POINT ( 'NONE',  ( -4.463089466550673734, 2.239389106484332981, 1.269702285208761605 ) ) ;
#12815=CARTESIAN_POINT ( 'NONE',  ( -3.450064735799886595, -4.100625000000076348, 0.3410961574374171690 ) ) ;
#12820=CARTESIAN_POINT ( 'NONE',  ( 2.598076211353310239, 1.678847577293378857, -4.499999999999999112 ) ) ;
#12827=DIRECTION ( 'NONE',  ( 2.551930889570659960E-15, -1.000000000000000000, -0.000000000000000000 ) ) ;
#12835=EDGE_LOOP ( 'NONE', ( #7101, #604 ) ) ;
#12836=CARTESIAN_POINT ( 'NONE',  ( -3.579691249134443698, -0.5937499999999900080, 2.390491442833416080 ) ) ;
#12838=CARTESIAN_POINT ( 'NONE',  ( -1.900756315137815067, -2.671088562373106434, 3.553810185735947869 ) ) ;
#12851=CARTESIAN_POINT ( 'NONE',  ( -3.686556889460768094, -0.1475000000000124822, 1.525885089196999056 ) ) ;
#12854=EDGE_CURVE ( 'NONE', #3303, #6571, #12216, .T. ) ;
#12855=CARTESIAN_POINT ( 'NONE',  ( 0.7224497989600745518, -2.366250000000003517, 3.625028471221638071 ) ) ;
#12861=DIRECTION ( 'NONE',  ( -1.224646799147353207E-16, -2.139562256385042123E-31, 1.000000000000000000 ) ) ;
#12870=CARTESIAN_POINT ( 'NONE',  ( -1.318845896519720506, -4.272500000000155396, 3.181678407182404467 ) ) ;
#12874=CARTESIAN_POINT ( 'NONE',  ( 0.7191817349834368489, -5.217963562372981201, -3.622537723569287493 ) ) ;
#12875=B_SPLINE_CURVE_WITH_KNOTS ( 'NONE', 3,
 ( #1082, #5402, #13614, #9380, #10170, #5471, #10460, #7868, #3134, #3487, #3413, #10543, #12444, #13684, #13760, #567, #2244, #6989, #4294, #3054, #12375, #15270, #1733, #4579, #5316, #2981, #12602, #9304, #14044, #14117, #12526, #6483, #9019, #6714, #11426, #14766, #4664, #1002, #8150, #12884, #11716, #11197, #10030, #4152, #8875, #1807, #9527, #1234, #4967, #8447, #2473, #2552, #11794, #1162, #2402, #2325, #8382, #10699, #7302, #3718, #67, #6157, #9676, #9450, #13123, #12963, #8667, #4818, #5921, #7073, #9605, #12030, #4734, #10622, #14270, #14189, #1399, #222, #10864, #3569, #148, #13192, #7221, #14410, #3649, #5994, #3796, #8303, #11944, #8527, #13044, #1311, #13273, #6075, #14340, #8223, #7151, #10786, #11872, #4900, #2145, #12775, #7956, #8271, #13012, #3460, #1132, #14012, #3388, #5658, #3226, #8190, #4635, #8038, #1049, #4548, #9353, #900, #9273, #10357, #13933, #15083, #3536, #4470, #9190, #974, #10280, #15009, #3304, #8121, #5893, #12855, #6892, #11610, #10595, #5727, #10429, #4709, #14093, #2215, #12928, #15158, #6958, #11680, #5805, #6736, #9421, #12694, #10511, #14160, #11764, #15317, #2066, #15239, #11456, #6816, #2290, #4400, #821, #7040, #5579, #9119, #13858, #11535, #14237, #10986, #13243, #6273, #3925, #7429, #9732, #10834, #13324, #6126, #14317, #5016, #8357, #3695, #8649, #7198, #14383, #2684, #12147, #10752, #8424, #2604, #4782, #7352, #4942, #9499, #13166, #3622, #2371, #7123, #14468, #1517, #9650, #3770, #1282, #13098, #3852, #2448, #11919, #6047, #196, #2523, #352, #8499, #5100, #11999, #117, #14543, #4868, #12080 ),
 .UNSPECIFIED., .F., .F.,
 ( 4, 2, 2, 2, 2, 2, 2, 2, 2, 2, 2, 2, 2, 2, 2, 2, 2, 2, 2, 2, 2, 2, 2, 2, 2, 2, 2, 2, 2, 2, 2, 2, 2, 2, 2, 2, 2, 2, 2, 2, 2, 2, 2, 2, 2, 2, 2, 2, 2, 2, 2, 2, 2, 2, 2, 2, 2, 2, 2, 2, 2, 2, 2, 2, 2, 2, 2, 2, 2, 2, 2, 2, 2, 2, 2, 2, 2, 2, 2, 2, 2, 2, 2, 2, 2, 2, 2, 2, 2, 2, 2, 2, 2, 2, 2, 2, 2, 2, 2, 2, 2, 2, 2, 2, 2, 2, 4 ),
 ( 0.1106917040526264190, 0.1171875000000000000, 0.1250000000000000000, 0.1328125000000000000, 0.1406250000000000000, 0.1484375000000000000, 0.1562500000000000000, 0.1640625000000000000, 0.1718750000000000000, 0.1796875000000000000, 0.1875000000000000000, 0.1953125000000000000, 0.2031250000000000000, 0.2109375000000000000, 0.2187500000000000000, 0.2265625000000000000, 0.2343750000000000000, 0.2421875000000000000, 0.2500000000000000000, 0.2578125000000000000, 0.2656250000000000000, 0.2734375000000000000, 0.2812500000000000000, 0.2890625000000000000, 0.2968750000000000000, 0.3046875000000000000, 0.3125000000000000000, 0.3203125000000000555, 0.3281250000000000000, 0.3359375000000000000, 0.3437500000000000000, 0.3515625000000000000, 0.3593750000000000000, 0.3671875000000000000, 0.3750000000000000000, 0.3828125000000000000, 0.3906250000000000000, 0.3984375000000000000, 0.4062500000000000000, 0.4140625000000000000, 0.4218750000000000000, 0.4296875000000000000, 0.4374999999999999445, 0.4453125000000000000, 0.4531250000000000000, 0.4609375000000000000, 0.4687500000000000000, 0.4765625000000000555, 0.4843750000000000000, 0.4921875000000000000, 0.5000000000000000000, 0.5078125000000000000, 0.5156250000000000000, 0.5234375000000000000, 0.5312500000000000000, 0.5390625000000000000, 0.5468750000000000000, 0.5546875000000000000, 0.5625000000000000000, 0.5703125000000000000, 0.5781250000000000000, 0.5859375000000000000, 0.5937500000000000000, 0.6015625000000001110, 0.6093750000000000000, 0.6171875000000000000, 0.6250000000000000000, 0.6328125000000000000, 0.6406250000000000000, 0.6484375000000000000, 0.6562500000000000000, 0.6640625000000000000, 0.6718750000000000000, 0.6796875000000000000, 0.6875000000000000000, 0.6953125000000000000, 0.7031250000000000000, 0.7109375000000000000, 0.7187500000000000000, 0.7265625000000000000, 0.7343750000000000000, 0.7421875000000000000, 0.7499999999999998890, 0.7578125000000000000, 0.7656250000000000000, 0.7734375000000000000, 0.7812500000000000000, 0.7890625000000001110, 0.7968750000000000000, 0.8046875000000000000, 0.8125000000000000000, 0.8203125000000000000, 0.8281250000000001110, 0.8359375000000000000, 0.8437500000000000000, 0.8515625000000000000, 0.8593750000000000000, 0.8671875000000001110, 0.8750000000000000000, 0.8828125000000000000, 0.8906250000000000000, 0.8984375000000000000, 0.9062500000000000000, 0.9140625000000000000, 0.9218749999999998890, 0.9296875000000000000, 0.9309053842486232355 ),
 .UNSPECIFIED. ) ;
#12884=CARTESIAN_POINT ( 'NONE',  ( 3.151910583997929116, -4.522499999999531894, 1.304188709559700232 ) ) ;
#12902=ORIENTED_EDGE ( 'NONE', *, *, #10785, .T. ) ;
#12905=CARTESIAN_POINT ( 'NONE',  ( 1.227202584385329587, -1.203124999999989342, -4.041673972266214498 ) ) ;
#12907=CARTESIAN_POINT ( 'NONE',  ( -0.7695070984847973694, -3.280463562373082009, -3.873892029236536416 ) ) ;
#12926=CARTESIAN_POINT ( 'NONE',  ( 3.049996619588438040, -0.4756250000000030176, 2.504408566260782010 ) ) ;
#12928=CARTESIAN_POINT ( 'NONE',  ( -3.284049251726958829, -2.163124999999908482, 1.754264853118110423 ) ) ;
#12931=DIRECTION ( 'NONE',  ( -1.000000000000000000, -1.747085166004344019E-15, 0.000000000000000000 ) ) ;
#12939=DIRECTION ( 'NONE',  ( 2.551930889570659960E-15, -1.000000000000000000, -0.000000000000000000 ) ) ;
#12941=ORIENTED_EDGE ( 'NONE', *, *, #10364, .T. ) ;
#12944=TOROIDAL_SURFACE ( 'NONE', #7748, -1.151041666666720031, 4.401041666666736241 ) ;
#12946=CARTESIAN_POINT ( 'NONE',  ( 0.6569748927284411177, -4.803749999999888054, -3.309289439050847381 ) ) ;
#12951=CARTESIAN_POINT ( 'NONE',  ( 3.837897214521031053, -3.983588562373158837, 0.3790132011682106339 ) ) ;
#12953=AXIS2_PLACEMENT_3D ( 'NONE', #7192, #1357, #11912 ) ;
#12956=CARTESIAN_POINT ( 'NONE',  ( 3.584540577507836603E-16, 9.015594676761164550, 0.000000000000000000 ) ) ;
#12963=CARTESIAN_POINT ( 'NONE',  ( -1.647113530155736916, -3.913124999999971099, -3.078783428963292490 ) ) ;
#12969=AXIS2_PLACEMENT_3D ( 'NONE', #13591, #696, #4266 ) ;
#12975=CARTESIAN_POINT ( 'NONE',  ( 1.342127543875233808, -3.772500000000060805, -3.243584335895732362 ) ) ;
#12977=CARTESIAN_POINT ( 'NONE',  ( 1.432789758436758154, -4.812499999999716671, 3.461605376534508505 ) ) ;
#12979=CARTESIAN_POINT ( 'NONE',  ( 1.555132164100668124, 2.118440305064532403, -4.499999999999999112 ) ) ;
#12982=DIRECTION ( 'NONE',  ( 9.422394424380278809E-16, -1.000000000000000000, 0.000000000000000000 ) ) ;
#12994=CARTESIAN_POINT ( 'NONE',  ( 4.056584590913882238, 0.06249999999998995942, 1.681565391176998769 ) ) ;
#12996=CARTESIAN_POINT ( 'NONE',  ( 4.061877285462823117, -1.046088562372976982, -1.233758211555065154 ) ) ;
#13004=DIRECTION ( 'NONE',  ( -0.1305261922200569580, 0.9914448613738096050, 0.000000000000000000 ) ) ;
#13005=DIRECTION ( 'NONE',  ( -0.8660254037844387076, -2.210036979070413080E-15, -0.4999999999999998890 ) ) ;
#13008=CARTESIAN_POINT ( 'NONE',  ( -0.3822054598150002591, -3.734374999999974243, 3.870204888229129114 ) ) ;
#13012=CARTESIAN_POINT ( 'NONE',  ( -3.184718056276182097, -3.006875000000130083, -1.703323619722481475 ) ) ;
#13018=DIRECTION ( 'NONE',  ( -1.000000000000000000, -2.622621077317916910E-15, 0.000000000000000000 ) ) ;
#13028=CARTESIAN_POINT ( 'NONE',  ( -2.894177851434075688, -3.991249999999941789, -1.934899151906828374 ) ) ;
#13031=EDGE_CURVE ( 'NONE', #1927, #4923, #63, .T. ) ;
#13033=CARTESIAN_POINT ( 'NONE',  ( 3.854459931122866223, -3.999213562372995856, -0.001409750848530770366 ) ) ;
#13039=CARTESIAN_POINT ( 'NONE',  ( -3.012508034349790975, 2.058119353682387409, 3.782183026296721540 ) ) ;
#13040=DIRECTION ( 'NONE',  ( 2.551930889570659960E-15, -1.000000000000000000, -0.000000000000000000 ) ) ;
#13044=CARTESIAN_POINT ( 'NONE',  ( -0.0009180086920793713474, -3.334999999999859632, 3.568205616840286698 ) ) ;
#13047=VERTEX_POINT ( 'NONE', #1745 ) ;
#13050=AXIS2_PLACEMENT_3D ( 'NONE', #11637, #1001, #8149 ) ;
#13052=CIRCLE ( 'NONE', #11074, 4.500000000000000888 ) ;
#13058=CARTESIAN_POINT ( 'NONE',  ( 1.033118776976089670, -3.381875000000070131, 3.408891928937246796 ) ) ;
#13065=CARTESIAN_POINT ( 'NONE',  ( 0.9018160986354060160, 2.304554878306184218, -4.499999999999999112 ) ) ;
#13075=ORIENTED_EDGE ( 'NONE', *, *, #6637, .F. ) ;
#13080=EDGE_CURVE ( 'NONE', #6471, #8682, #12150, .T. ) ;
#13081=CARTESIAN_POINT ( 'NONE',  ( -0.001183910938090454099, 0.2499999999998853417, 4.416106207682124918 ) ) ;
#13083=CARTESIAN_POINT ( 'NONE',  ( 1.204928114531795158, -1.796088562373254982, 3.966944375248610655 ) ) ;
#13089=ORIENTED_EDGE ( 'NONE', *, *, #8192, .F. ) ;
#13095=CARTESIAN_POINT ( 'NONE',  ( -3.506684959068008034, -4.437500000000057732, -1.453587443624275499 ) ) ;
#13097=VECTOR ( 'NONE', #10061, 1000.000000000000000 ) ;
#13098=CARTESIAN_POINT ( 'NONE',  ( 1.493882881115753847, -0.7724999999999562217, -3.610279343491855641 ) ) ;
#13105=AXIS2_PLACEMENT_3D ( 'NONE', #10597, #4714, #13018 ) ;
#13112=CARTESIAN_POINT ( 'NONE',  ( -0.7073002561900944007, -2.866249999999988418, -3.560643744722165938 ) ) ;
#13123=CARTESIAN_POINT ( 'NONE',  ( -2.211816241884709822, -3.944375000000018172, -2.696513105594267046 ) ) ;
#13125=VERTEX_POINT ( 'NONE', #8295 ) ;
#13128=ORIENTED_EDGE ( 'NONE', *, *, #13702, .T. ) ;
#13131=CARTESIAN_POINT ( 'NONE',  ( 0.3508518002069317410, -3.350624999999907150, 3.548798009676430887 ) ) ;
#13137=DIRECTION ( 'NONE',  ( 1.000000000000000000, 9.422394424380278809E-16, 0.000000000000000000 ) ) ;
#13151=CARTESIAN_POINT ( 'NONE',  ( 2.995266967284331283, -1.124213562373126862, -2.993673064536260142 ) ) ;
#13158=EDGE_LOOP ( 'NONE', ( #350, #6909, #652, #7015 ) ) ;
#13160=B_SPLINE_CURVE_WITH_KNOTS ( 'NONE', 3,
 ( #5547, #5468, #14978, #10166, #1888, #4371, #10101, #14834, #7934, #4218, #11354, #5315, #10029, #3052, #3131, #11502, #9094, #8942, #12524, #4446, #720, #564, #2036, #6643, #867, #9165, #13904, #14900, #8004, #1732 ),
 .UNSPECIFIED., .F., .F.,
 ( 4, 2, 2, 2, 2, 2, 2, 2, 2, 2, 2, 2, 2, 2, 4 ),
 ( 0.000000000000000000, 0.0006682858881741897015, 0.001336571776348379403, 0.002004857664522568996, 0.002673143552696758806, 0.003341429440870947749, 0.004009715329045136258, 0.004678001217219326067, 0.005346287105393515010, 0.006014572993567703953, 0.006682858881741892028, 0.007351144769916080970, 0.008019430658090269046, 0.009356002434438646931, 0.01069257421078702308 ),
 .UNSPECIFIED. ) ;
#13164=CARTESIAN_POINT ( 'NONE',  ( -2.667345689317278890, -4.625000000000156319, 2.665957393838279010 ) ) ;
#13166=CARTESIAN_POINT ( 'NONE',  ( -3.224082633657694430, -0.9912500000000042943, -2.155484159616896989 ) ) ;
#13170=CARTESIAN_POINT ( 'NONE',  ( 0.000000000000000000, 0.000000000000000000, 0.000000000000000000 ) ) ;
#13171=CARTESIAN_POINT ( 'NONE',  ( 3.406229051843177036, -5.265617073852581598, 0.7216417731445288197 ) ) ;
#13179=CARTESIAN_POINT ( 'NONE',  ( 1.974738715674900114, -3.428749999999933795, 2.957050713271640152 ) ) ;
#13186=CARTESIAN_POINT ( 'NONE',  ( -2.802265715718426975, 1.883037081658663903, 4.146333404067328310 ) ) ;
#13192=CARTESIAN_POINT ( 'NONE',  ( 3.389189273868536745, -3.538124999999807674, 1.026728768593236030 ) ) ;
#13203=CARTESIAN_POINT ( 'NONE',  ( 0.3421672931281763419, -3.819374999999898268, -3.487344533451358863 ) ) ;
#13204=CARTESIAN_POINT ( 'NONE',  ( -6.060835862730317059E-15, 2.375000000000000000, 0.000000000000000000 ) ) ;
#13205=CARTESIAN_POINT ( 'NONE',  ( -0.3668491701747607636, -4.734375000000160760, 3.738752075031570588 ) ) ;
#13223=CARTESIAN_POINT ( 'NONE',  ( -2.388143517671037941, -0.6554635623729724303, 3.572045695433365697 ) ) ;
#13240=CARTESIAN_POINT ( 'NONE',  ( 1.432789758436758154, -4.812499999999716671, 3.461605376534508505 ) ) ;
#13243=CARTESIAN_POINT ( 'NONE',  ( 3.730555813499059070, -1.553749999999926246, 0.7430650243616524486 ) ) ;
#13245=AXIS2_PLACEMENT_3D ( 'NONE', #9193, #4788, #5730 ) ;
#13246=EDGE_CURVE ( 'NONE', #11128, #12756, #7095, .T. ) ;
#13247=CARTESIAN_POINT ( 'NONE',  ( 0.1494771202956585165, -5.386673054885917189, 3.320955697048893818 ) ) ;
#13251=CARTESIAN_POINT ( 'NONE',  ( 3.267958496119054423, -5.289367998540840610, 1.137001996541352034 ) ) ;
#13262=ORIENTED_EDGE ( 'NONE', *, *, #13386, .T. ) ;
#13265=CARTESIAN_POINT ( 'NONE',  ( -3.265322824347066444, -5.249359343367779651, -1.273401769415555496 ) ) ;
#13272=B_SPLINE_CURVE_WITH_KNOTS ( 'NONE', 3,
 ( #1802, #15055, #641, #13681 ),
 .UNSPECIFIED., .F., .F.,
 ( 4, 4 ),
 ( 0.002598307151460989804, 0.005196383362814306975 ),
 .UNSPECIFIED. ) ;
#13273=CARTESIAN_POINT ( 'NONE',  ( -1.038475776471825762, -3.288125000000012843, 3.420226703972062854 ) ) ;
#13274=CARTESIAN_POINT ( 'NONE',  ( -2.598076211353316012, 0.1227504548087343245, -4.499999999999999112 ) ) ;
#13277=ORIENTED_EDGE ( 'NONE', *, *, #12447, .T. ) ;
#13285=CARTESIAN_POINT ( 'NONE',  ( 3.109021928378527200, -3.663124999999927578, -1.660781358202984448 ) ) ;
#13286=CARTESIAN_POINT ( 'NONE',  ( 3.701456747302541928, -5.015624999999988454, -0.3659357139933352987 ) ) ;
#13288=DIRECTION ( 'NONE',  ( -1.000000000000000000, -2.551930889570659960E-15, 0.000000000000000000 ) ) ;
#13291=CIRCLE ( 'NONE', #14990, 3.173335668876520188 ) ;
#13293=DIRECTION ( 'NONE',  ( -1.000000000000000000, -2.551930889570659565E-15, 0.000000000000000000 ) ) ;
#13302=CARTESIAN_POINT ( 'NONE',  ( -1.520556115814812870, -5.913125000000218456, -2.846480943363819627 ) ) ;
#13304=CARTESIAN_POINT ( 'NONE',  ( 3.856928834949548079, -0.07812500000007562007, -2.060244425025098192 ) ) ;
#13306=CARTESIAN_POINT ( 'NONE',  ( -3.858379451542089278, -1.561713562373104214, 1.599828451265935536 ) ) ;
#13311=FACE_OUTER_BOUND ( 'NONE', #2441, .T. ) ;
#13320=CARTESIAN_POINT ( 'NONE',  ( -3.138285373062238648, -4.593749999999839240, 2.098600886432549828 ) ) ;
#13321=ORIENTED_EDGE ( 'NONE', *, *, #6742, .F. ) ;
#13322=CARTESIAN_POINT ( 'NONE',  ( 1.089607726473704297, -4.796088562373097552, 3.587212734375584411 ) ) ;
#13324=CARTESIAN_POINT ( 'NONE',  ( 1.801006600569655891, -1.413124999999811449, 3.371562913404185569 ) ) ;
#13325=CARTESIAN_POINT ( 'NONE',  ( -2.598076211353319120, 1.678847577293364424, 4.500000000000000888 ) ) ;
#13331=CARTESIAN_POINT ( 'NONE',  ( -2.320576762250993852, 9.355654565435171932, 3.410994500647662804E-16 ) ) ;
#13336=ORIENTED_EDGE ( 'NONE', *, *, #6717, .T. ) ;
#13337=ORIENTED_EDGE ( 'NONE', *, *, #14835, .F. ) ;
#13342=CARTESIAN_POINT ( 'NONE',  ( 3.244093391032127016, -2.506875000000020837, 1.732468392772113841 ) ) ;
#13347=CARTESIAN_POINT ( 'NONE',  ( 0.7350389054958545998, -5.152513402290675337, -3.570507098978675131 ) ) ;
#13358=ORIENTED_EDGE ( 'NONE', *, *, #8726, .T. ) ;
#13363=CARTESIAN_POINT ( 'NONE',  ( -3.093239089446854884, -2.178749999999916476, 2.068481483294962953 ) ) ;
#13364=CARTESIAN_POINT ( 'NONE',  ( 0.3862366009532263167, -3.234374999999897859, -3.936230821419137271 ) ) ;
#13377=UNCERTAINTY_MEASURE_WITH_UNIT (LENGTH_MEASURE( 1.000000000000000082E-05 ), #11146, 'distance_accuracy_value', 'NONE');
#13378=CARTESIAN_POINT ( 'NONE',  ( -0.3227798623957894852, -5.319375000000161613, 3.289865787063878777 ) ) ;
#13380=CARTESIAN_POINT ( 'NONE',  ( -3.199287326323787095, -5.038124999999881837, -0.9691876696830878934 ) ) ;
#13386=EDGE_CURVE ( 'NONE', #6471, #14595, #2048, .T. ) ;
#13390=ORIENTED_EDGE ( 'NONE', *, *, #514, .T. ) ;
#13391=CARTESIAN_POINT ( 'NONE',  ( 0.4017167453136591404, -2.234374999999921396, -4.067671435978028605 ) ) ;
#13393=CARTESIAN_POINT ( 'NONE',  ( -3.159664717618257956, -4.405463562373036268, -2.112412258076255878 ) ) ;
#13408=CARTESIAN_POINT ( 'NONE',  ( -2.931404194366994176, 4.650702586819535966, 0.000000000000000000 ) ) ;
#13409=CARTESIAN_POINT ( 'NONE',  ( 0.001402937982463629916, -1.335000000000034825, 3.832736870811305874 ) ) ;
#13417=AXIS2_PLACEMENT_3D ( 'NONE', #1763, #14631, #2937 ) ;
#13418=CARTESIAN_POINT ( 'NONE',  ( 2.348303809467377601, -0.4995676945082530018, -3.345954089472160664 ) ) ;
#13435=PLANE ( 'NONE',  #115 ) ;
#13436=CARTESIAN_POINT ( 'NONE',  ( -2.115018882620673057, -4.343749999999819700, -3.167137413913937660 ) ) ;
#13439=ADVANCED_FACE ( 'NONE', ( #6190 ), #8999, .T. ) ;
#13454=CARTESIAN_POINT ( 'NONE',  ( 3.013463120154617148, -5.647500000000105658, -1.249542180252701806 ) ) ;
#13456=CARTESIAN_POINT ( 'NONE',  ( 0.9404171202240950711, -5.788124999999990195, -3.104336352551607892 ) ) ;
#13469=DIRECTION ( 'NONE',  ( 1.000000000000000000, 0.000000000000000000, -6.982962677686266711E-15 ) ) ;
#13470=CARTESIAN_POINT ( 'NONE',  ( 1.163914675889782702, -2.796875000000069722, 3.840555497293599352 ) ) ;
#13471=EDGE_LOOP ( 'NONE', ( #10731, #7707, #13651, #5820, #14965, #14668 ) ) ;
#13472=AXIS2_PLACEMENT_3D ( 'NONE', #14744, #1791, #11404 ) ;
#13478=CARTESIAN_POINT ( 'NONE',  ( -0.9013897961777794787, 2.290928418211087614, 4.500000000000000888 ) ) ;
#13487=CARTESIAN_POINT ( 'NONE',  ( 2.100337907687724215, -1.741249999999995968, -3.141606438102673149 ) ) ;
#13494=CARTESIAN_POINT ( 'NONE',  ( -4.763139720814411504, 0.04639863247562014958, -0.7500000000000002220 ) ) ;
#13495=CARTESIAN_POINT ( 'NONE',  ( -4.296227084909979510, -0.4995677573761841406, -0.01166785054812304046 ) ) ;
#13510=CARTESIAN_POINT ( 'NONE',  ( -1.439523803302256155, -1.897500000000171383, -3.471712813344601578 ) ) ;
#13511=DIRECTION ( 'NONE',  ( 9.422394424380278809E-16, -1.000000000000000000, 0.000000000000000000 ) ) ;
#13513=CARTESIAN_POINT ( 'NONE',  ( -3.506684959068008034, -4.437500000000057732, -1.453587443624275499 ) ) ;
#13518=CARTESIAN_POINT ( 'NONE',  ( 1.243192046278082774, -0.7968750000001610934, 4.092941397521737912 ) ) ;
#13535=EDGE_CURVE ( 'NONE', #6571, #953, #10972, .T. ) ;
#13536=CARTESIAN_POINT ( 'NONE',  ( 2.063655046872799215, -5.725624999999673115, -2.513280214060358286 ) ) ;
#13537=DIRECTION ( 'NONE',  ( -1.000000000000000000, -1.724434379501977811E-15, 0.000000000000000000 ) ) ;
#13539=CARTESIAN_POINT ( 'NONE',  ( -5.196152422706636465, 2.374999999999986677, -8.561039196169309507E-16 ) ) ;
#13555=CARTESIAN_POINT ( 'NONE',  ( -0.001482159116125898214, -2.249999999999994227, -4.085353063378265759 ) ) ;
#13567=ORIENTED_EDGE ( 'NONE', *, *, #13797, .F. ) ;
#13569=CARTESIAN_POINT ( 'NONE',  ( -0.3703630857573827484, -1.850625000000086562, -3.746264557426809638 ) ) ;
#13575=CARTESIAN_POINT ( 'NONE',  ( 3.558919284812731565, -0.4995676945082496712, -1.914344080127182268 ) ) ;
#13583=EDGE_LOOP ( 'NONE', ( #10199, #3238, #3632, #229, #6137 ) ) ;
#13589=CARTESIAN_POINT ( 'NONE',  ( -2.598076211353321341, 2.374999999999993339, -4.499999999999999112 ) ) ;
#13590=CARTESIAN_POINT ( 'NONE',  ( -1.775679308629948050, -4.671875000000182077, 3.319983975552966537 ) ) ;
#13591=CARTESIAN_POINT ( 'NONE',  ( -9.797174393178927223E-17, 9.500000000000000000, 0.000000000000000000 ) ) ;
#13595=CARTESIAN_POINT ( 'NONE',  ( -0.8118119174735605181, -1.718749999999964917, 4.075604227461077755 ) ) ;
#13606=CARTESIAN_POINT ( 'NONE',  ( -1.562933739280453205, -5.256875000000181153, 2.922265072135110220 ) ) ;
#13608=CARTESIAN_POINT ( 'NONE',  ( -1.673688575075004152E-15, 4.650702586819541295, 0.000000000000000000 ) ) ;
#13614=CARTESIAN_POINT ( 'NONE',  ( 1.208453367980061088, -5.394866591894509789, 3.060934444180607450 ) ) ;
#13621=CARTESIAN_POINT ( 'NONE',  ( 3.905735209131758534, -3.031249999999969802, -0.7758307200683374205 ) ) ;
#13623=CARTESIAN_POINT ( 'NONE',  ( -0.001018162134759268388, -3.749213562372953223, 3.887570876297712363 ) ) ;
#13627=CARTESIAN_POINT ( 'NONE',  ( 1.732658076282566739, 0.04645217140505895209, -4.499999999999999112 ) ) ;
#13630=EDGE_CURVE ( 'NONE', #4633, #13125, #11485, .T. ) ;
#13631=CARTESIAN_POINT ( 'NONE',  ( -1.770063184917655574, 2.057215485424180201, 4.500000000000000888 ) ) ;
#13639=CARTESIAN_POINT ( 'NONE',  ( 2.123627735229572266, -1.428750000000023501, 3.175715285003386956 ) ) ;
#13643=CARTESIAN_POINT ( 'NONE',  ( -1.673688575075004152E-15, 4.650702586819541295, 0.000000000000000000 ) ) ;
#13645=CARTESIAN_POINT ( 'NONE',  ( -4.091800360845128992, -0.4995676945082698217, -1.248354756450685832 ) ) ;
#13651=ORIENTED_EDGE ( 'NONE', *, *, #1373, .T. ) ;
#13655=CARTESIAN_POINT ( 'NONE',  ( 0.3539834606289790075, -5.764838562372911923, 3.603588891846962738 ) ) ;
#13656=CARTESIAN_POINT ( 'NONE',  ( -3.284049251726958829, -2.163124999999908482, 1.754264853118110423 ) ) ;
#13658=CARTESIAN_POINT ( 'NONE',  ( 3.820852842225918700, -2.953124999999806821, 1.157524667501716786 ) ) ;
#13662=CARTESIAN_POINT ( 'NONE',  ( -4.100362740845592491, -1.531249999999860556, 0.8144810970459482879 ) ) ;
#13673=EDGE_CURVE ( 'NONE', #4034, #8371, #13160, .T. ) ;
#13676=CARTESIAN_POINT ( 'NONE',  ( 2.085982869228583780, -5.444374999999953779, 2.543086608318696928 ) ) ;
#13681=CARTESIAN_POINT ( 'NONE',  ( -2.598076211353316012, 0.1227504548087343245, -4.499999999999999112 ) ) ;
#13683=CARTESIAN_POINT ( 'NONE',  ( 1.151041666666722030, 7.362500000000001599, 0.000000000000000000 ) ) ;
#13684=CARTESIAN_POINT ( 'NONE',  ( -3.186695398571379290, -5.131874999999967990, 0.9679749472946410638 ) ) ;
#13692=CARTESIAN_POINT ( 'NONE',  ( -3.563986660466321510, -2.578124999999990230, 1.906655726273616125 ) ) ;
#13694=AXIS2_PLACEMENT_3D ( 'NONE', #7315, #10714, #10800 ) ;
#13701=CARTESIAN_POINT ( 'NONE',  ( 2.598076211353311127, 1.678847577293378190, 4.500000000000000000 ) ) ;
#13702=EDGE_CURVE ( 'NONE', #7247, #8682, #944, .T. ) ;
#13703=CARTESIAN_POINT ( 'NONE',  ( 0.8000000000000123679, 8.384405323238834029, 9.797174393178965434E-17 ) ) ;
#13712=CARTESIAN_POINT ( 'NONE',  ( -1.470831194960215083, -1.272500000000085230, 3.548278161707651535 ) ) ;
#13716=VECTOR ( 'NONE', #1793, 1000.000000000000114 ) ;
#13733=CARTESIAN_POINT ( 'NONE',  ( 2.288508625327937640, -5.858588562373046926, 2.790022829016634454 ) ) ;
#13734=CARTESIAN_POINT ( 'NONE',  ( 3.931950937192209228, -0.5849999999998678479, -0.001434051515494208940 ) ) ;
#13736=CARTESIAN_POINT ( 'NONE',  ( 2.515861257320511246, -3.140624999999957367, -3.067863912704874796 ) ) ;
#13739=AXIS2_PLACEMENT_3D ( 'NONE', #1988, #6671, #11156 ) ;
#13742=CARTESIAN_POINT ( 'NONE',  ( 4.228334800557012940, -1.015625000000088818, -0.4153177470898732904 ) ) ;
#13753=CARTESIAN_POINT ( 'NONE',  ( -0.6836773592642079178, -3.866249999999994635, -3.430425219284937821 ) ) ;
#13758=DIRECTION ( 'NONE',  ( -1.000000000000000000, 0.000000000000000000, 0.000000000000000000 ) ) ;
#13760=CARTESIAN_POINT ( 'NONE',  ( -3.268702447147800783, -5.116250000000009734, 0.6493246907702930892 ) ) ;
#13768=CARTESIAN_POINT ( 'NONE',  ( -2.335396930795095471, -1.343749999999818368, -3.497180482087419051 ) ) ;
#13783=CIRCLE ( 'NONE', #6370, 0.8600000000000014300 ) ;
#13787=CARTESIAN_POINT ( 'NONE',  ( -1.872693635133553691, -0.2568750000000157852, 3.506634376076540160 ) ) ;
#13790=AXIS2_PLACEMENT_3D ( 'NONE', #8568, #7498, #14310 ) ;
#13797=EDGE_CURVE ( 'NONE', #6270, #8132, #10014, .T. ) ;
#13807=ORIENTED_EDGE ( 'NONE', *, *, #1726, .F. ) ;
#13809=CARTESIAN_POINT ( 'NONE',  ( -1.388373139153629587, -5.686713562372827546, 3.355330185783546249 ) ) ;
#13811=CARTESIAN_POINT ( 'NONE',  ( -3.844997831300932756, -1.100624999999974429, 0.3801187285354425405 ) ) ;
#13813=CARTESIAN_POINT ( 'NONE',  ( -3.752022838101215285, -2.437499999999895195, -1.552542887664947635 ) ) ;
#13819=CARTESIAN_POINT ( 'NONE',  ( -2.948053448091068507, -1.625000000000079936, 2.946489148067756858 ) ) ;
#13830=CARTESIAN_POINT ( 'NONE',  ( 0.9808155824294413350, -4.788124999999903153, -3.230360883553721862 ) ) ;
#13843=CARTESIAN_POINT ( 'NONE',  ( 4.228334800557012940, -1.015625000000088818, -0.4153177470898732904 ) ) ;
#13845=CARTESIAN_POINT ( 'NONE',  ( 3.965348895242338134, -3.014838562373144182, -0.3920103835965588757 ) ) ;
#13855=CARTESIAN_POINT ( 'NONE',  ( -2.595824455272694564, -5.375000000000100364, -2.597168749630690332 ) ) ;
#13858=CARTESIAN_POINT ( 'NONE',  ( 3.503209385669602938, -1.647500000000019948, -1.450007420588620866 ) ) ;
#13859=CARTESIAN_POINT ( 'NONE',  ( -0.8655643756568760505, -2.519089588807311881E-15, -4.499999999999999112 ) ) ;
#13863=CARTESIAN_POINT ( 'NONE',  ( 3.372444421885775423, -0.4995676945082423992, 2.006840812041871924 ) ) ;
#13866=CARTESIAN_POINT ( 'NONE',  ( -3.081487911019577365E-30, 0.000000000000000000, 0.000000000000000000 ) ) ;
#13868=CARTESIAN_POINT ( 'NONE',  ( -2.598076211353315568, 0.1227504548087345604, 4.500000000000000888 ) ) ;
#13875=CARTESIAN_POINT ( 'NONE',  ( -3.492279824153255330, -5.546088562373062025, 1.060777629467175132 ) ) ;
#13876=CARTESIAN_POINT ( 'NONE',  ( 2.481497852716095132, -0.7256250000000298295, -3.025965195089417747 ) ) ;
#13879=CARTESIAN_POINT ( 'NONE',  ( -3.563986660466321510, -2.578124999999990230, 1.906655726273616125 ) ) ;
#13884=DIRECTION ( 'NONE',  ( -9.422394424380278809E-16, 1.000000000000000000, -0.000000000000000000 ) ) ;
#13895=CARTESIAN_POINT ( 'NONE',  ( -0.3313405146688110925, -4.850625000000119869, -3.351331461923120703 ) ) ;
#13898=CARTESIAN_POINT ( 'NONE',  ( 0.000000000000000000, 0.000000000000000000, 0.000000000000000000 ) ) ;
#13899=CARTESIAN_POINT ( 'NONE',  ( 2.598076211353315124, 0.1227504548087477720, 4.500000000000000000 ) ) ;
#13900=CARTESIAN_POINT ( 'NONE',  ( 1.771711357391134500, 2.042612654333142430, -4.500000000000000000 ) ) ;
#13904=CARTESIAN_POINT ( 'NONE',  ( -3.884436258901674766, -0.4995676945082689335, 1.749149344944205042 ) ) ;
#13908=CARTESIAN_POINT ( 'NONE',  ( -3.637955631634631981, -5.500000000000012434, -2.540370839878330420E-14 ) ) ;
#13911=CARTESIAN_POINT ( 'NONE',  ( 0.8000000000000113687, 9.500000000000000000, 9.797174393178965434E-17 ) ) ;
#13912=ORIENTED_EDGE ( 'NONE', *, *, #346, .F. ) ;
#13913=CIRCLE ( 'NONE', #2258, 2.577850803773722443 ) ;
#13914=CARTESIAN_POINT ( 'NONE',  ( -1.221455774822097329, -1.296874999999898082, -4.030457444822014956 ) ) ;
#13916=CARTESIAN_POINT ( 'NONE',  ( -0.001440864359646425088, -3.249213562373088227, -3.953673997506742754 ) ) ;
#13917=AXIS2_PLACEMENT_3D ( 'NONE', #8172, #7248, #7329 ) ;
#13925=CARTESIAN_POINT ( 'NONE',  ( 7.511572993685698521E-16, 1.916901515185129432E-30, 4.500000000000000888 ) ) ;
#13930=CARTESIAN_POINT ( 'NONE',  ( -2.814361612698371484, -0.2100000000001143730, 2.816411668391418210 ) ) ;
#13933=CARTESIAN_POINT ( 'NONE',  ( 3.503842902704710216, -2.631874999999911147, -1.061889326425361268 ) ) ;
#13945=CARTESIAN_POINT ( 'NONE',  ( 1.614039610742502795, -4.413124999999970655, 3.021508266705728030 ) ) ;
#13951=CARTESIAN_POINT ( 'NONE',  ( 1.801006600569655891, -1.413124999999811449, 3.371562913404185569 ) ) ;
#13954=CARTESIAN_POINT ( 'NONE',  ( -2.264039642164870969, -2.343749999999985789, -3.385713959793517080 ) ) ;
#13961=FACE_OUTER_BOUND ( 'NONE', #5861, .T. ) ;
#13967=VERTEX_POINT ( 'NONE', #7474 ) ;
#13971=CONICAL_SURFACE ( 'NONE', #13739, 3.173335668876520632, 0.9162978572970248425 ) ;
#13989=DIRECTION ( 'NONE',  ( -9.422394424380278809E-16, 1.000000000000000000, -0.000000000000000000 ) ) ;
#13991=CARTESIAN_POINT ( 'NONE',  ( 3.738955316585249822, -1.078124999999896527, -2.000248979885406619 ) ) ;
#13993=CARTESIAN_POINT ( 'NONE',  ( -3.466325857683220324, -3.421088562373224562, -1.853959688331944244 ) ) ;
#13998=CARTESIAN_POINT ( 'NONE',  ( 2.598076211353310239, 1.678847577293378857, -4.499999999999999112 ) ) ;
#14009=CARTESIAN_POINT ( 'NONE',  ( -0.7612222386588008982, -0.8662499999999671019, -3.819631723157197012 ) ) ;
#14012=CARTESIAN_POINT ( 'NONE',  ( -2.013335231365204425, -2.928749999999985310, -3.010762893885847280 ) ) ;
#14015=FACE_OUTER_BOUND ( 'NONE', #4959, .T. ) ;
#14026=CARTESIAN_POINT ( 'NONE',  ( 3.333123593314366584, -4.616249999999967990, -0.6642911394208930176 ) ) ;
#14032=CARTESIAN_POINT ( 'NONE',  ( -2.041896248660992175, -5.342963562372913700, -3.057627329919577086 ) ) ;
#14034=CARTESIAN_POINT ( 'NONE',  ( 0.3898743713140499501, -0.3506250000000236122, 3.943731105175205975 ) ) ;
#14035=CARTESIAN_POINT ( 'NONE',  ( -2.598076211353321341, 2.374999999999993339, -4.499999999999999112 ) ) ;
#14038=DIRECTION ( 'NONE',  ( -2.551930889570659960E-15, 1.000000000000000000, 0.000000000000000000 ) ) ;
#14044=CARTESIAN_POINT ( 'NONE',  ( 0.9808155824294413350, -4.788124999999903153, -3.230360883553721862 ) ) ;
#14048=ORIENTED_EDGE ( 'NONE', *, *, #9491, .F. ) ;
#14054=CARTESIAN_POINT ( 'NONE',  ( 0.6569748927284305706, -4.803749999999888054, -3.309289439050846937 ) ) ;
#14072=CARTESIAN_POINT ( 'NONE',  ( 2.992932217727461097, -1.124999999999971800, -2.995094308971279151 ) ) ;
#14075=CARTESIAN_POINT ( 'NONE',  ( 4.097285757785106952, -2.014838562373181485, -0.4024520375138228578 ) ) ;
#14090=CARTESIAN_POINT ( 'NONE',  ( 0.3898743713140983003, -0.3506250000000236122, 3.943731105175303231 ) ) ;
#14093=CARTESIAN_POINT ( 'NONE',  ( -2.629016928070645243, -2.210000000000078568, 2.627652665972809665 ) ) ;
#14097=CARTESIAN_POINT ( 'NONE',  ( 6.205964732515537312E-15, 4.927357795815634489, 0.000000000000000000 ) ) ;
#14108=CARTESIAN_POINT ( 'NONE',  ( -1.068188678435922245, -5.296088562372957220, -3.524632553026846082 ) ) ;
#14117=CARTESIAN_POINT ( 'NONE',  ( 1.592243150387700146, -4.756875000000070131, -2.981552405995577359 ) ) ;
#14124=CARTESIAN_POINT ( 'NONE',  ( -2.533829858540697977, -3.209999999999945786, 2.535703909530142575 ) ) ;
#14138=DIRECTION ( 'NONE',  ( -6.860497997771531562E-15, -6.464231808267455010E-30, -1.000000000000000000 ) ) ;
#14140=CARTESIAN_POINT ( 'NONE',  ( 4.382995262527464853, 1.326351951446563815E-13, -0.001575499653098922336 ) ) ;
#14142=CARTESIAN_POINT ( 'NONE',  ( 3.934944799906381796, -0.9367135623731039917, 1.631135842912540879 ) ) ;
#14147=CARTESIAN_POINT ( 'NONE',  ( 3.452158817763105070, 2.307268873417427368, -3.020685531837379312 ) ) ;
#14150=CARTESIAN_POINT ( 'NONE',  ( -3.173335668876506865, -5.500000000000010658, 0.000000000000000000 ) ) ;
#14155=ADVANCED_FACE ( 'NONE', ( #14872 ), #7231, .T. ) ;
#14157=CARTESIAN_POINT ( 'NONE',  ( -1.491583768208377681, -3.687499999999984901, 3.598334897712680114 ) ) ;
#14160=CARTESIAN_POINT ( 'NONE',  ( -2.381388125886219509, -1.944375000000168052, -2.899558211763606064 ) ) ;
#14162=EDGE_CURVE ( 'NONE', #1380, #13125, #12252, .T. ) ;
#14170=FACE_OUTER_BOUND ( 'NONE', #6142, .T. ) ;
#14179=CARTESIAN_POINT ( 'NONE',  ( 3.272906902298228005, -5.077338562373189923, -1.750952971977949968 ) ) ;
#14189=CARTESIAN_POINT ( 'NONE',  ( 2.928286698324767290, -3.678750000000110987, -1.958188979435658839 ) ) ;
#14200=CARTESIAN_POINT ( 'NONE',  ( -1.707523105661799434, -2.913124999999936904, -3.196535590052164810 ) ) ;
#14221=CARTESIAN_POINT ( 'NONE',  ( 4.165833326811591242, -1.030463562373184150, -0.8274826639205559164 ) ) ;
#14224=CARTESIAN_POINT ( 'NONE',  ( 2.802265715718417205, 1.883037081658679446, -4.146333404067327422 ) ) ;
#14230=CARTESIAN_POINT ( 'NONE',  ( 3.519594483087749914, -5.184756082317176329, -0.7836709140574362742 ) ) ;
#14232=SHAPE_DEFINITION_REPRESENTATION ( #4883, #4448 ) ;
#14234=CARTESIAN_POINT ( 'NONE',  ( -3.618276846414829162, -4.546874999999968914, 1.099041561241040466 ) ) ;
#14237=CARTESIAN_POINT ( 'NONE',  ( 3.779448512589415721, -1.600625000000089226, -0.3712484392070565797 ) ) ;
#14244=DIRECTION ( 'NONE',  ( -1.000000000000000000, -2.459952698498907323E-15, 0.000000000000000000 ) ) ;
#14254=CARTESIAN_POINT ( 'NONE',  ( 2.255458548909141214, -3.444374999999939568, 2.746210667320787557 ) ) ;
#14256=ORIENTED_EDGE ( 'NONE', *, *, #15102, .T. ) ;
#14270=CARTESIAN_POINT ( 'NONE',  ( 2.488663048653545928, -3.709999999999854303, -2.487386788893799494 ) ) ;
#14274=AXIS2_PLACEMENT_3D ( 'NONE', #14389, #9969, #1372 ) ;
#14275=ORIENTED_EDGE ( 'NONE', *, *, #8062, .F. ) ;
#14282=CARTESIAN_POINT ( 'NONE',  ( 1.055499318045234114, -2.788125000000055476, -3.484140247641438926 ) ) ;
#14290=CARTESIAN_POINT ( 'NONE',  ( 2.320576762250993852, 9.355654565435175485, 0.000000000000000000 ) ) ;
#14299=AXIS2_PLACEMENT_3D ( 'NONE', #14364, #2659, #6179 ) ;
#14301=CARTESIAN_POINT ( 'NONE',  ( -1.284862778419491258, 0.2968750000000271450, 4.231539792689364532 ) ) ;
#14303=CARTESIAN_POINT ( 'NONE',  ( -4.109106552884008501, -1.467963562373030717, -0.8158076774038809376 ) ) ;
#14310=DIRECTION ( 'NONE',  ( 1.000000000000000000, 2.551930889570660354E-15, 0.000000000000000000 ) ) ;
#14314=CARTESIAN_POINT ( 'NONE',  ( -3.331846864947428877, -4.578125000000028422, 1.779793940175935729 ) ) ;
#14317=CARTESIAN_POINT ( 'NONE',  ( 0.7459506331255062461, -1.366249999999944897, 3.755271276440939054 ) ) ;
#14330=CARTESIAN_POINT ( 'NONE',  ( -3.166267757014364914, -3.163124999999988862, 1.693910156975117154 ) ) ;
#14340=CARTESIAN_POINT ( 'NONE',  ( -1.990045403832418236, -3.241250000000046594, 2.976654046991286329 ) ) ;
#14351=CARTESIAN_POINT ( 'NONE',  ( 3.376561219002149450, -3.631875000000035048, -1.025635141340205836 ) ) ;
#14357=ADVANCED_FACE ( 'NONE', ( #7447 ), #4477, .T. ) ;
#14364=CARTESIAN_POINT ( 'NONE',  ( -1.006616814747114065E-29, -2.568816543514387226E-44, 0.000000000000000000 ) ) ;
#14371=CARTESIAN_POINT ( 'NONE',  ( 2.684023608889491985, -1.139838562373123310, -3.272901415737858422 ) ) ;
#14372=CARTESIAN_POINT ( 'NONE',  ( 6.205964732515537312E-15, 4.927357795815634489, 0.000000000000000000 ) ) ;
#14381=CARTESIAN_POINT ( 'NONE',  ( -3.849008435184475996, -3.468750000000023093, -0.7641557335396481632 ) ) ;
#14383=CARTESIAN_POINT ( 'NONE',  ( -2.441443777772203561, -1.225625000000065912, 2.973322847374053612 ) ) ;
#14389=CARTESIAN_POINT ( 'NONE',  ( -1.096602777094355814E-14, 4.297149196226271783, 0.000000000000000000 ) ) ;
#14394=LINE ( 'NONE', #3783, #4322 ) ;
#14395=CARTESIAN_POINT ( 'NONE',  ( -3.335258087793214088, -3.022499999999893827, -1.380066378191329379 ) ) ;
#14402=CARTESIAN_POINT ( 'NONE',  ( -3.412007067234435809, -5.260309433033398818, -0.7367663078464588011 ) ) ;
#14410=CARTESIAN_POINT ( 'NONE',  ( 2.950365215318619949, -3.491249999999835651, 1.969791294043586660 ) ) ;
#14433=VECTOR ( 'NONE', #12187, 999.9999999999998863 ) ;
#14440=EDGE_LOOP ( 'NONE', ( #426, #3531 ) ) ;
#14442=CARTESIAN_POINT ( 'NONE',  ( -1.266249875242109635, -5.272499999999733511, 3.060236832100307058 ) ) ;
#14446=CARTESIAN_POINT ( 'NONE',  ( 2.372463320875326520, -0.8429635623729573313, 3.552691932206611281 ) ) ;
#14465=CARTESIAN_POINT ( 'NONE',  ( 3.553279128418493915, -4.062500000000332179, -1.470728592776388455 ) ) ;
#14467=CARTESIAN_POINT ( 'NONE',  ( 3.776578263379590350, -4.030463562373150843, -0.7501819099998634499 ) ) ;
#14468=CARTESIAN_POINT ( 'NONE',  ( -1.487946254897619447, -0.8975000000000187272, -3.594883137563858355 ) ) ;
#14474=FACE_OUTER_BOUND ( 'NONE', #7503, .T. ) ;
#14482=CARTESIAN_POINT ( 'NONE',  ( -1.707523105661755025, -2.913124999999936904, -3.196535590052165254 ) ) ;
#14486=CARTESIAN_POINT ( 'NONE',  ( -0.1886744959232814767, -5.170134308371691745, -3.603086115839904569 ) ) ;
#14489=CARTESIAN_POINT ( 'NONE',  ( -2.397583379056643427, -0.4995676945082651588, -3.461308205639501256 ) ) ;
#14498=ORIENTED_EDGE ( 'NONE', *, *, #8169, .F. ) ;
#14502=CARTESIAN_POINT ( 'NONE',  ( 3.244093391032126572, -2.506875000000020837, 1.732468392772068544 ) ) ;
#14504=DIRECTION ( 'NONE',  ( -1.000000000000000000, -2.505711687522054122E-15, 0.000000000000000000 ) ) ;
#14505=CARTESIAN_POINT ( 'NONE',  ( -3.849008435184475996, -3.468750000000023093, -0.7641557335396481632 ) ) ;
#14519=CARTESIAN_POINT ( 'NONE',  ( 2.709518412118975483, -5.678749999999861409, -1.809455179588199014 ) ) ;
#14523=CARTESIAN_POINT ( 'NONE',  ( -2.103997734759339711, -5.225624999999808118, 2.565685703212198021 ) ) ;
#14538=DIRECTION ( 'NONE',  ( -6.982962677686266711E-15, -6.579622859988665673E-30, -1.000000000000000000 ) ) ;
#14539=CARTESIAN_POINT ( 'NONE',  ( -3.970076885172157066, -2.531249999999920064, 0.7911966920917139490 ) ) ;
#14541=CARTESIAN_POINT ( 'NONE',  ( 1.742702564072879046, -5.171088562373163278, -3.263254631422885854 ) ) ;
#14543=CARTESIAN_POINT ( 'NONE',  ( 3.432145566543734372, -0.5044392315027305118, 1.902605341171852427 ) ) ;
#14545=AXIS2_PLACEMENT_3D ( 'NONE', #13643, #1051, #12931 ) ;
#14561=CARTESIAN_POINT ( 'NONE',  ( -0.0009180086920682582752, -3.334999999999859632, 3.568205616840287142 ) ) ;
#14567=CARTESIAN_POINT ( 'NONE',  ( -3.198284477310383789, -5.245703666927238551, -1.445171886050707011 ) ) ;
#14579=ORIENTED_EDGE ( 'NONE', *, *, #13535, .T. ) ;
#14583=CARTESIAN_POINT ( 'NONE',  ( 1.514604053328734823, -3.187500000000060396, -3.660349086209866876 ) ) ;
#14585=CARTESIAN_POINT ( 'NONE',  ( 0.8667276783654334071, 2.116104415309936157E-15, 4.500000000000000000 ) ) ;
#14586=CARTESIAN_POINT ( 'NONE',  ( -4.342069816296838525, 2.307268873417408273, -1.479314468162620466 ) ) ;
#14589=CARTESIAN_POINT ( 'NONE',  ( 1.274862231047225439E-15, -0.4995676945082591081, 0.000000000000000000 ) ) ;
#14595=VERTEX_POINT ( 'NONE', #5425 ) ;
#14596=ORIENTED_EDGE ( 'NONE', *, *, #2953, .F. ) ;
#14597=CARTESIAN_POINT ( 'NONE',  ( -0.6299995022919476773, -5.866249999999999964, -3.171388681290751688 ) ) ;
#14607=FACE_OUTER_BOUND ( 'NONE', #12383, .T. ) ;
#14610=FILL_AREA_STYLE ('',( #1674 ) ) ;
#14611=CARTESIAN_POINT ( 'NONE',  ( 3.325473450044490242, -2.906249999999835243, 2.220260485081660740 ) ) ;
#14612=ORIENTED_EDGE ( 'NONE', *, *, #1287, .T. ) ;
#14615=DIRECTION ( 'NONE',  ( -9.422394424380278809E-16, 1.000000000000000000, -0.000000000000000000 ) ) ;
#14616=EDGE_CURVE ( 'NONE', #11643, #11128, #4440, .T. ) ;
#14621=CARTESIAN_POINT ( 'NONE',  ( 1.274862231047225439E-15, -0.4995676945082591081, 0.000000000000000000 ) ) ;
#14627=CARTESIAN_POINT ( 'NONE',  ( -3.717546150574278840, -2.069374999999891607, -0.3671215460811527720 ) ) ;
#14631=DIRECTION ( 'NONE',  ( -2.551930889570660354E-15, 1.000000000000000000, 0.000000000000000000 ) ) ;
#14633=CARTESIAN_POINT ( 'NONE',  ( 2.252671702316018543, -5.120840197140201333, -2.900062017644191581 ) ) ;
#14655=CARTESIAN_POINT ( 'NONE',  ( -1.750120246539625946, -2.256875000000012843, 3.272202384321437840 ) ) ;
#14657=CARTESIAN_POINT ( 'NONE',  ( -3.920035875790600421, -3.499999999999977796, -0.001028343392498549860 ) ) ;
#14660=DIRECTION ( 'NONE',  ( -9.422394424380278809E-16, 1.000000000000000000, -0.000000000000000000 ) ) ;
#14662=CARTESIAN_POINT ( 'NONE',  ( -5.196152422706636465, 2.374999999999986677, -8.561039196169309507E-16 ) ) ;
#14668=ORIENTED_EDGE ( 'NONE', *, *, #1342, .T. ) ;
#14673=ORIENTED_EDGE ( 'NONE', *, *, #13630, .T. ) ;
#14679=CARTESIAN_POINT ( 'NONE',  ( 2.937061643673781752, -5.103115294876279684, -2.234448363260541193 ) ) ;
#14682=CIRCLE ( 'NONE', #7025, 4.500000000000000888 ) ;
#14689=CARTESIAN_POINT ( 'NONE',  ( -0.001059456894846966344, -2.749999999999859224, 4.019249942169077272 ) ) ;
#14695=CARTESIAN_POINT ( 'NONE',  ( 5.196152422706624918, 2.375000000000013323, -1.265134450516282343E-15 ) ) ;
#14706=CARTESIAN_POINT ( 'NONE',  ( -3.693744850241972522, -1.131875000000025722, 1.119430425315800282 ) ) ;
#14707=ORIENTED_EDGE ( 'NONE', *, *, #6345, .F. ) ;
#14711=EDGE_CURVE ( 'NONE', #3303, #9311, #797, .T. ) ;
#14714=CARTESIAN_POINT ( 'NONE',  ( -0.6343012717231791830, -0.4995676945082608289, -4.116477779236263679 ) ) ;
#14717=CIRCLE ( 'NONE', #8035, 0.5000000000000000000 ) ;
#14730=CARTESIAN_POINT ( 'NONE',  ( 3.779448512589415721, -1.600625000000089226, -0.3712484392070565797 ) ) ;
#14736=CARTESIAN_POINT ( 'NONE',  ( 3.783699349552338997, -3.968750000000262013, 0.7536532579988950431 ) ) ;
#14740=CARTESIAN_POINT ( 'NONE',  ( -3.980019242547642833, -0.5625000000000109912, 1.650257999534034514 ) ) ;
#14744=CARTESIAN_POINT ( 'NONE',  ( 3.584540577507836603E-16, 9.015594676761164550, 0.000000000000000000 ) ) ;
#14756=CARTESIAN_POINT ( 'NONE',  ( 3.124039007639229037, -5.631874999999973319, -0.9468071286117496488 ) ) ;
#14766=CARTESIAN_POINT ( 'NONE',  ( 3.333123593314366140, -4.616249999999967990, -0.6642911394208504960 ) ) ;
#14772=CARTESIAN_POINT ( 'NONE',  ( -2.852666340614860463, -2.624999999999946265, 2.854740429567705018 ) ) ;
#14780=CARTESIAN_POINT ( 'NONE',  ( -2.193587568837934931, 1.881091898551119135, 4.500000000000000888 ) ) ;
#14786=CARTESIAN_POINT ( 'NONE',  ( -3.224082633657789465, -0.9912500000000042943, -2.155484159616802398 ) ) ;
#14806=CARTESIAN_POINT ( 'NONE',  ( 3.647531283552059023, -2.600625000000050591, -0.3606074429803771131 ) ) ;
#14809=CARTESIAN_POINT ( 'NONE',  ( 2.991150664073139342, -3.890625000000195399, 2.452944570972435567 ) ) ;
#14813=CARTESIAN_POINT ( 'NONE',  ( -1.643569066580401916, -0.6875000000000854872, 3.964934652274553439 ) ) ;
#14823=ORIENTED_EDGE ( 'NONE', *, *, #3081, .F. ) ;
#14826=CARTESIAN_POINT ( 'NONE',  ( -0.3227798623957894297, -5.319375000000161613, 3.289865787063878333 ) ) ;
#14829=ADVANCED_FACE ( 'NONE', ( #6103 ), #2263, .T. ) ;
#14834=CARTESIAN_POINT ( 'NONE',  ( 1.824979221380550021, -0.4995676945082544451, 3.571726915116150813 ) ) ;
#14835=EDGE_CURVE ( 'NONE', #6571, #9068, #9945, .T. ) ;
#14836=CARTESIAN_POINT ( 'NONE',  ( -2.931404194366994176, 4.650702586819535966, 0.000000000000000000 ) ) ;
#14842=CARTESIAN_POINT ( 'NONE',  ( 2.623679764461153141, -1.859375000000051070, 3.198691315062023310 ) ) ;
#14848=FACE_OUTER_BOUND ( 'NONE', #8469, .T. ) ;
#14856=CARTESIAN_POINT ( 'NONE',  ( 3.503209385669603382, -1.647500000000019948, -1.450007420588574680 ) ) ;
#14859=FACE_OUTER_BOUND ( 'NONE', #13471, .T. ) ;
#14860=CARTESIAN_POINT ( 'NONE',  ( -1.543400882162985400E-14, 7.839999999999998082, 5.619086434621074034E-29 ) ) ;
#14872=FACE_OUTER_BOUND ( 'NONE', #1756, .T. ) ;
#14873=CARTESIAN_POINT ( 'NONE',  ( 1.916065064279496746E-15, 7.362499999999997158, 0.000000000000000000 ) ) ;
#14876=CARTESIAN_POINT ( 'NONE',  ( 4.118464008547413790, -2.000000000000003109, 0.001090570402295849319 ) ) ;
#14877=CARTESIAN_POINT ( 'NONE',  ( 2.598076211353314235, 0.1227504548087474667, -4.499999999999999112 ) ) ;
#14880=CARTESIAN_POINT ( 'NONE',  ( -4.125408418587476866, -0.5468750000000269784, 1.250226324283678192 ) ) ;
#14894=CARTESIAN_POINT ( 'NONE',  ( -3.069066067673428932, -4.006874999999906706, -1.638984897852511891 ) ) ;
#14898=CARTESIAN_POINT ( 'NONE',  ( 5.196152422706626695, 1.678847577293385296, -1.115338501812287204E-15 ) ) ;
#14900=CARTESIAN_POINT ( 'NONE',  ( -4.193021748915730207, -0.4995676945082699327, 0.9078562877249845009 ) ) ;
#14908=EDGE_CURVE ( 'NONE', #953, #9311, #7961, .T. ) ;
#14911=CARTESIAN_POINT ( 'NONE',  ( -2.727692609523614475, -0.6406250000000671685, 3.321895092029963248 ) ) ;
#14915=CARTESIAN_POINT ( 'NONE',  ( -2.759584380001296910, -3.624213562373039377, 2.761600069345273134 ) ) ;
#14929=ADVANCED_FACE ( 'NONE', ( #10892 ), #8801, .T. ) ;
#14931=CARTESIAN_POINT ( 'NONE',  ( -2.896649075160178111, -1.975624999999826548, -2.378478989283399958 ) ) ;
#14948=CARTESIAN_POINT ( 'NONE',  ( 3.124039007639229482, -5.631874999999973319, -0.9468071286117497598 ) ) ;
#14952=CARTESIAN_POINT ( 'NONE',  ( 1.704156345177410881, -5.827338562373107322, 3.185422574234377358 ) ) ;
#14953=CARTESIAN_POINT ( 'NONE',  ( 3.459076575081923899, -0.6631250000000769029, -1.847748348019847109 ) ) ;
#14955=CARTESIAN_POINT ( 'NONE',  ( -1.185531852251327400, -2.296875000000050182, -3.903075577084617720 ) ) ;
#14965=ORIENTED_EDGE ( 'NONE', *, *, #1576, .F. ) ;
#14967=ORIENTED_EDGE ( 'NONE', *, *, #12386, .F. ) ;
#14968=VERTEX_POINT ( 'NONE', #6184 ) ;
#14973=CARTESIAN_POINT ( 'NONE',  ( -2.894177851434075244, -3.991249999999941789, -1.934899151906914305 ) ) ;
#14978=CARTESIAN_POINT ( 'NONE',  ( 3.141122330734205104, -0.4995676945082517251, 2.389792696361102919 ) ) ;
#14983=CARTESIAN_POINT ( 'NONE',  ( 2.919796888921922573, -5.104126807837104707, -2.256669152708658643 ) ) ;
#14988=CARTESIAN_POINT ( 'NONE',  ( 2.013502677559834808, -0.8281249999998109290, 3.769415173278118480 ) ) ;
#14990=AXIS2_PLACEMENT_3D ( 'NONE', #3820, #11965, #8546 ) ;
#14991=CARTESIAN_POINT ( 'NONE',  ( -0.4017660263608561211, -2.264838562373181041, -4.064082169119537902 ) ) ;
#14993=AXIS2_PLACEMENT_3D ( 'NONE', #5250, #3153, #6433 ) ;
#15006=CARTESIAN_POINT ( 'NONE',  ( -2.210630411551929519, -0.2412499999998789502, 3.306558829207998595 ) ) ;
#15009=CARTESIAN_POINT ( 'NONE',  ( 2.605880849243368491, -2.459999999999848086, 2.603962797083386072 ) ) ;
#15030=ORIENTED_EDGE ( 'NONE', *, *, #11251, .T. ) ;
#15031=CARTESIAN_POINT ( 'NONE',  ( -3.215696830464670697, -5.577338562373121533, 1.717757276957577073 ) ) ;
#15032=CARTESIAN_POINT ( 'NONE',  ( -2.441443777772203561, -1.225625000000065912, 2.973322847374053612 ) ) ;
#15034=CARTESIAN_POINT ( 'NONE',  ( 3.303237764219515427, -3.093750000000110578, -2.208893390251179589 ) ) ;
#15038=CARTESIAN_POINT ( 'NONE',  ( 2.598076211353311127, 1.678847577293378190, 4.500000000000000000 ) ) ;
#15046=ORIENTED_EDGE ( 'NONE', *, *, #13535, .F. ) ;
#15051=CARTESIAN_POINT ( 'NONE',  ( 3.009749400183384882, -4.506874999999939568, 1.609730366092098075 ) ) ;
#15053=CARTESIAN_POINT ( 'NONE',  ( 2.598076211353308462, 2.375000000000006661, -4.499999999999999112 ) ) ;
#15055=CARTESIAN_POINT ( 'NONE',  ( -3.464101615137753054, -9.090049444189458401E-15, -2.999999999999999112 ) ) ;
#15066=CARTESIAN_POINT ( 'NONE',  ( -0.4056240317154969355, -1.734374999999933831, 4.133709567805635920 ) ) ;
#15068=CARTESIAN_POINT ( 'NONE',  ( 1.148110318453624545, -3.202338562373148623, -3.789782819255727020 ) ) ;
#15080=CARTESIAN_POINT ( 'NONE',  ( 0.3626941743317158018, -5.234374999999986677, -3.672738340478102437 ) ) ;
#15083=CARTESIAN_POINT ( 'NONE',  ( 3.647531283552059023, -2.600625000000050591, -0.3606074429803771131 ) ) ;
#15089=FACE_OUTER_BOUND ( 'NONE', #9612, .T. ) ;
#15100=CARTESIAN_POINT ( 'NONE',  ( 1.981854314971675413, -6.155463562373256536, -2.968431064909258232 ) ) ;
#15101=CARTESIAN_POINT ( 'NONE',  ( 1.493882881115753847, -0.7724999999999562217, -3.610279343491855641 ) ) ;
#15102=EDGE_CURVE ( 'NONE', #13967, #5514, #7492, .T. ) ;
#15103=CARTESIAN_POINT ( 'NONE',  ( -3.466497813382189541, -5.275048774667015827, -7.182839392716466875E-16 ) ) ;
#15104=CARTESIAN_POINT ( 'NONE',  ( 0.3952026422296860964, -2.765624999999906741, 3.997656568947202338 ) ) ;
#15109=DIRECTION ( 'NONE',  ( -1.000000000000000000, -1.067522139062645149E-15, 0.000000000000000000 ) ) ;
#15120=CARTESIAN_POINT ( 'NONE',  ( 1.903042727507366250, -4.428749999999965326, 2.845810502761935368 ) ) ;
#15138=CARTESIAN_POINT ( 'NONE',  ( -1.643569066580401916, -0.6875000000000854872, 3.964934652274553439 ) ) ;
#15140=CARTESIAN_POINT ( 'NONE',  ( 2.202232363153947770, -3.155463562373067798, -3.298474133106217288 ) ) ;
#15149=DIRECTION ( 'NONE',  ( -1.000000000000000000, -2.551930889570659960E-15, 0.000000000000000000 ) ) ;
#15154=CARTESIAN_POINT ( 'NONE',  ( 3.459076575081828864, -0.6631250000000769029, -1.847748348019894848 ) ) ;
#15158=CARTESIAN_POINT ( 'NONE',  ( -3.566427039428707868, -2.131875000000089670, 1.083295335393480219 ) ) ;
#15172=CARTESIAN_POINT ( 'NONE',  ( 3.009749400183385326, -4.506874999999939568, 1.609730366092140708 ) ) ;
#15179=CARTESIAN_POINT ( 'NONE',  ( 2.432356863550838355, -4.139838562373138409, -2.966048421176934458 ) ) ;
#15180=CARTESIAN_POINT ( 'NONE',  ( 1.515516452534992897, -0.3975000000001072675, 3.655012690611888715 ) ) ;
#15183=CARTESIAN_POINT ( 'NONE',  ( -1.169542390366794304, -2.703125000000013323, 3.851808151836873861 ) ) ;
#15186=CARTESIAN_POINT ( 'NONE',  ( 3.663887442738342770, 2.356280171323993589, 2.653960795963570707 ) ) ;
#15208=CARTESIAN_POINT ( 'NONE',  ( 4.330127018922191873, 1.087837616813861542E-14, -1.500000000000001332 ) ) ;
#15223=CARTESIAN_POINT ( 'NONE',  ( 4.035539303778883813, -2.030463562373035380, -0.8042393191121177676 ) ) ;
#15236=CARTESIAN_POINT ( 'NONE',  ( 3.104176526174651229, -4.906250000000120792, 2.075311058921220919 ) ) ;
#15239=CARTESIAN_POINT ( 'NONE',  ( -0.3703630857574056745, -1.850625000000086340, -3.746264557426716379 ) ) ;
#15241=AXIS2_PLACEMENT_3D ( 'NONE', #1331, #1419, #13293 ) ;
#15244=FACE_OUTER_BOUND ( 'NONE', #10158, .T. ) ;
#15257=AXIS2_PLACEMENT_3D ( 'NONE', #2739, #1506, #334 ) ;
#15258=CARTESIAN_POINT ( 'NONE',  ( -3.767882347484534211, -4.514838562373170383, 0.3724990980822453501 ) ) ;
#15270=CARTESIAN_POINT ( 'NONE',  ( -2.129528971937844517, -4.944374999999755715, -2.592863122870853410 ) ) ;
#15291=ORIENTED_EDGE ( 'NONE', *, *, #5571, .T. ) ;
#15294=VECTOR ( 'NONE', #12422, 1000.000000000000000 ) ;
#15296=DIRECTION ( 'NONE',  ( -1.000000000000000000, 0.000000000000000000, 6.860497997771530774E-15 ) ) ;
#15301=CARTESIAN_POINT ( 'NONE',  ( 3.324617108750066663, -2.905463562373210351, 2.222704761906319160 ) ) ;
#15315=CARTESIAN_POINT ( 'NONE',  ( -1.733052192687106308, -5.328125000000219380, -3.244333203286712042 ) ) ;
#15317=CARTESIAN_POINT ( 'NONE',  ( -1.439523803302256155, -1.897500000000171383, -3.471712813344601578 ) ) ;
#15329=CARTESIAN_POINT ( 'NONE',  ( 0.6686498792469652841, -4.366249999999815223, 3.366016213005436519 ) ) ;
#15333=CARTESIAN_POINT ( 'NONE',  ( -1.441154219919537516, -4.686713562373249431, 3.476695106718095118 ) ) ;
#15334=DIRECTION ( 'NONE',  ( -1.000000000000000000, -1.067522139062645149E-15, 0.000000000000000000 ) ) ;
#15335=ORIENTED_EDGE ( 'NONE', *, *, #888, .T. ) ;
ENDSEC;
END-ISO-10303-21;
